ISO-10303-21;
HEADER;
/* Generated by software containing ST-Developer
 * from STEP Tools, Inc. (www.steptools.com) 
 */

FILE_DESCRIPTION(
/* description */ ('Independent keyed three-contact power inlet for the IEC-connector des
ign category. Longer ground blade, retained contacts, wire termination
 holes and sealed bolted panel interface. Nominal custom interface; IE
C dimensional compatibility and electrical ratings are not assigned.'),

/* implementation_level */ '2;1');

FILE_NAME(
/* name */ 'Socket head cap screw M4x8.step',
/* time_stamp */ '2026-11-08T19:55:04-08:00',
/* author */ (''),
/* organization */ (''),
/* preprocessor_version */ 'ST-DEVELOPER v20.2',
/* originating_system */ 'Autodesk Translation Framework v15.17.0.0',
/* authorisation */ '');

FILE_SCHEMA (('AUTOMOTIVE_DESIGN { 1 0 10303 214 3 1 1 }'));
ENDSEC;

DATA;
#10=MECHANICAL_DESIGN_GEOMETRIC_PRESENTATION_REPRESENTATION('',(#115),#21880);
#79=CONICAL_SURFACE('',#6845,1.5,0.785398163397448);
#95=SHAPE_REPRESENTATION_RELATIONSHIP('SRR','None',#21931,#105);
#105=ADVANCED_BREP_SHAPE_REPRESENTATION('',(#125),#21876);
#115=STYLED_ITEM('',(#21986),#125);
#125=MANIFOLD_SOLID_BREP('Body1',#6387);
#137=B_SPLINE_SURFACE_WITH_KNOTS('',3,3,((#17361,#17362,#17363,#17364,#17365,
#17366,#17367,#17368,#17369,#17370,#17371,#17372,#17373,#17374,#17375,#17376,
#17377,#17378,#17379,#17380,#17381,#17382,#17383,#17384,#17385,#17386,#17387,
#17388,#17389,#17390,#17391,#17392,#17393,#17394,#17395,#17396,#17397,#17398,
#17399,#17400,#17401,#17402,#17403,#17404,#17405,#17406,#17407,#17408,#17409,
#17410,#17411,#17412,#17413,#17414,#17415,#17416,#17417,#17418,#17419,#17420,
#17421,#17422,#17423,#17424,#17425,#17426,#17427,#17428,#17429,#17430),
(#17431,#17432,#17433,#17434,#17435,#17436,#17437,#17438,#17439,#17440,
#17441,#17442,#17443,#17444,#17445,#17446,#17447,#17448,#17449,#17450,#17451,
#17452,#17453,#17454,#17455,#17456,#17457,#17458,#17459,#17460,#17461,#17462,
#17463,#17464,#17465,#17466,#17467,#17468,#17469,#17470,#17471,#17472,#17473,
#17474,#17475,#17476,#17477,#17478,#17479,#17480,#17481,#17482,#17483,#17484,
#17485,#17486,#17487,#17488,#17489,#17490,#17491,#17492,#17493,#17494,#17495,
#17496,#17497,#17498,#17499,#17500),(#17501,#17502,#17503,#17504,#17505,
#17506,#17507,#17508,#17509,#17510,#17511,#17512,#17513,#17514,#17515,#17516,
#17517,#17518,#17519,#17520,#17521,#17522,#17523,#17524,#17525,#17526,#17527,
#17528,#17529,#17530,#17531,#17532,#17533,#17534,#17535,#17536,#17537,#17538,
#17539,#17540,#17541,#17542,#17543,#17544,#17545,#17546,#17547,#17548,#17549,
#17550,#17551,#17552,#17553,#17554,#17555,#17556,#17557,#17558,#17559,#17560,
#17561,#17562,#17563,#17564,#17565,#17566,#17567,#17568,#17569,#17570),
(#17571,#17572,#17573,#17574,#17575,#17576,#17577,#17578,#17579,#17580,
#17581,#17582,#17583,#17584,#17585,#17586,#17587,#17588,#17589,#17590,#17591,
#17592,#17593,#17594,#17595,#17596,#17597,#17598,#17599,#17600,#17601,#17602,
#17603,#17604,#17605,#17606,#17607,#17608,#17609,#17610,#17611,#17612,#17613,
#17614,#17615,#17616,#17617,#17618,#17619,#17620,#17621,#17622,#17623,#17624,
#17625,#17626,#17627,#17628,#17629,#17630,#17631,#17632,#17633,#17634,#17635,
#17636,#17637,#17638,#17639,#17640)),.UNSPECIFIED.,.F.,.F.,.F.,(4,4),(4,
1,1,1,1,1,1,1,1,1,1,1,1,1,1,1,1,1,1,1,1,1,1,1,1,1,1,1,1,1,1,1,1,1,1,1,1,
1,1,1,1,1,1,1,1,1,1,1,1,1,1,1,1,1,1,1,1,1,1,1,1,1,1,1,1,1,1,4),(0.,0.0460148164544132),
(11.6154215191106,12.6127599630189,13.6100984069272,14.6074368508354,15.6047752947437,
16.602113738652,17.5994521825603,18.5967906264686,19.5941290703769,20.5914675142851,
21.5888059581934,22.5861444021017,23.58348284601,24.5808212899183,25.5781597338266,
26.5754981777348,27.5728366216431,28.5701750655514,29.5675135094597,30.564851953368,
31.5621903972762,32.5595288411845,33.5568672850928,34.5542057290011,35.5515441729094,
36.5488826168177,37.5462210607259,38.5435595046342,39.5408979485425,40.5382363924508,
41.5355748363591,42.5329132802674,43.5302517241756,44.5275901680839,45.5249286119922,
46.5222670559005,47.5196054998088,48.516943943717,49.5142823876253,50.5116208315336,
51.5089592754419,52.5062977193502,53.5036361632585,54.5009746071667,55.498313051075,
56.4956514949833,57.4929899388916,58.4903283827999,59.4876668267081,60.4850052706164,
61.4823437145247,62.479682158433,63.4770206023413,64.4743590462496,65.4716974901578,
66.4690359340661,67.4663743779744,68.4637128218827,69.461051265791,70.4583897096992,
71.4557281536075,72.4530665975158,73.4504050414241,74.4477434853324,75.4450819292407,
76.4424203731489,77.4397588170572,78.4370972609655),.UNSPECIFIED.);
#138=B_SPLINE_SURFACE_WITH_KNOTS('',3,3,((#17766,#17767,#17768,#17769,#17770,
#17771,#17772,#17773,#17774,#17775,#17776,#17777,#17778,#17779,#17780,#17781,
#17782,#17783,#17784,#17785,#17786,#17787,#17788,#17789,#17790,#17791,#17792,
#17793,#17794,#17795,#17796,#17797,#17798,#17799,#17800,#17801,#17802,#17803,
#17804,#17805,#17806,#17807,#17808,#17809,#17810,#17811,#17812,#17813,#17814,
#17815,#17816,#17817,#17818,#17819,#17820,#17821,#17822,#17823,#17824,#17825,
#17826,#17827,#17828,#17829,#17830,#17831,#17832,#17833,#17834,#17835,#17836,
#17837),(#17838,#17839,#17840,#17841,#17842,#17843,#17844,#17845,#17846,
#17847,#17848,#17849,#17850,#17851,#17852,#17853,#17854,#17855,#17856,#17857,
#17858,#17859,#17860,#17861,#17862,#17863,#17864,#17865,#17866,#17867,#17868,
#17869,#17870,#17871,#17872,#17873,#17874,#17875,#17876,#17877,#17878,#17879,
#17880,#17881,#17882,#17883,#17884,#17885,#17886,#17887,#17888,#17889,#17890,
#17891,#17892,#17893,#17894,#17895,#17896,#17897,#17898,#17899,#17900,#17901,
#17902,#17903,#17904,#17905,#17906,#17907,#17908,#17909),(#17910,#17911,
#17912,#17913,#17914,#17915,#17916,#17917,#17918,#17919,#17920,#17921,#17922,
#17923,#17924,#17925,#17926,#17927,#17928,#17929,#17930,#17931,#17932,#17933,
#17934,#17935,#17936,#17937,#17938,#17939,#17940,#17941,#17942,#17943,#17944,
#17945,#17946,#17947,#17948,#17949,#17950,#17951,#17952,#17953,#17954,#17955,
#17956,#17957,#17958,#17959,#17960,#17961,#17962,#17963,#17964,#17965,#17966,
#17967,#17968,#17969,#17970,#17971,#17972,#17973,#17974,#17975,#17976,#17977,
#17978,#17979,#17980,#17981),(#17982,#17983,#17984,#17985,#17986,#17987,
#17988,#17989,#17990,#17991,#17992,#17993,#17994,#17995,#17996,#17997,#17998,
#17999,#18000,#18001,#18002,#18003,#18004,#18005,#18006,#18007,#18008,#18009,
#18010,#18011,#18012,#18013,#18014,#18015,#18016,#18017,#18018,#18019,#18020,
#18021,#18022,#18023,#18024,#18025,#18026,#18027,#18028,#18029,#18030,#18031,
#18032,#18033,#18034,#18035,#18036,#18037,#18038,#18039,#18040,#18041,#18042,
#18043,#18044,#18045,#18046,#18047,#18048,#18049,#18050,#18051,#18052,#18053)),
 .UNSPECIFIED.,.F.,.F.,.F.,(4,4),(4,1,1,1,1,1,1,1,1,1,1,1,1,1,1,1,1,1,1,
1,1,1,1,1,1,1,1,1,1,1,1,1,1,1,1,1,1,1,1,1,1,1,1,1,1,1,1,1,1,1,1,1,1,1,1,
1,1,1,1,1,1,1,1,1,1,1,1,1,1,4),(0.,0.0460148164544132),(8.31058692273974,
9.30894657310399,10.3073062234682,11.3056658738325,12.3040255241967,13.302385174561,
14.3007448249252,15.2991044752895,16.2974641256537,17.295823776018,18.2941834263822,
19.2925430767465,20.2909027271107,21.289262377475,22.2876220278392,23.2859816782034,
24.2843413285677,25.2827009789319,26.2810606292962,27.2794202796604,28.2777799300247,
29.2761395803889,30.2744992307532,31.2728588811174,32.2712185314817,33.2695781818459,
34.2679378322102,35.2662974825744,36.2646571329387,37.2630167833029,38.2613764336672,
39.2597360840314,40.2580957343957,41.2564553847599,42.2548150351241,43.2531746854884,
44.2515343358526,45.2498939862169,46.2482536365811,47.2466132869454,48.2449729373096,
49.2433325876739,50.2416922380381,51.2400518884024,52.2384115387666,53.2367711891309,
54.2351308394951,55.2334904898594,56.2318501402236,57.2302097905879,58.2285694409521,
59.2269290913164,60.2252887416806,61.2236483920448,62.2220080424091,63.2203676927733,
64.2187273431376,65.2170869935018,66.2154466438661,67.2138062942303,68.2121659445946,
69.2105255949588,70.2088852453231,71.2072448956873,72.2056045460516,73.2039641964158,
74.2023238467801,75.2006834971443,76.1990431475085,77.1974027978728),
 .UNSPECIFIED.);
#189=FACE_BOUND('',#984,.T.);
#190=FACE_BOUND('',#987,.T.);
#283=PLANE('',#6851);
#284=PLANE('',#6852);
#285=PLANE('',#6853);
#286=PLANE('',#6854);
#287=PLANE('',#6855);
#288=PLANE('',#6856);
#289=PLANE('',#6857);
#290=PLANE('',#6858);
#291=PLANE('',#6862);
#292=PLANE('',#6863);
#561=FACE_OUTER_BOUND('',#951,.T.);
#562=FACE_OUTER_BOUND('',#952,.T.);
#563=FACE_OUTER_BOUND('',#953,.T.);
#564=FACE_OUTER_BOUND('',#954,.T.);
#565=FACE_OUTER_BOUND('',#955,.T.);
#566=FACE_OUTER_BOUND('',#956,.T.);
#567=FACE_OUTER_BOUND('',#957,.T.);
#568=FACE_OUTER_BOUND('',#958,.T.);
#569=FACE_OUTER_BOUND('',#959,.T.);
#570=FACE_OUTER_BOUND('',#960,.T.);
#571=FACE_OUTER_BOUND('',#961,.T.);
#572=FACE_OUTER_BOUND('',#962,.T.);
#573=FACE_OUTER_BOUND('',#963,.T.);
#574=FACE_OUTER_BOUND('',#964,.T.);
#575=FACE_OUTER_BOUND('',#965,.T.);
#576=FACE_OUTER_BOUND('',#966,.T.);
#577=FACE_OUTER_BOUND('',#967,.T.);
#578=FACE_OUTER_BOUND('',#968,.T.);
#579=FACE_OUTER_BOUND('',#969,.T.);
#580=FACE_OUTER_BOUND('',#970,.T.);
#581=FACE_OUTER_BOUND('',#971,.T.);
#582=FACE_OUTER_BOUND('',#972,.T.);
#583=FACE_OUTER_BOUND('',#973,.T.);
#584=FACE_OUTER_BOUND('',#974,.T.);
#585=FACE_OUTER_BOUND('',#975,.T.);
#586=FACE_OUTER_BOUND('',#976,.T.);
#587=FACE_OUTER_BOUND('',#977,.T.);
#588=FACE_OUTER_BOUND('',#978,.T.);
#589=FACE_OUTER_BOUND('',#979,.T.);
#590=FACE_OUTER_BOUND('',#980,.T.);
#591=FACE_OUTER_BOUND('',#981,.T.);
#592=FACE_OUTER_BOUND('',#982,.T.);
#593=FACE_OUTER_BOUND('',#983,.T.);
#594=FACE_OUTER_BOUND('',#985,.T.);
#595=FACE_OUTER_BOUND('',#986,.T.);
#596=FACE_OUTER_BOUND('',#988,.T.);
#951=EDGE_LOOP('',(#5255,#5256,#5257,#5258));
#952=EDGE_LOOP('',(#5259,#5260,#5261,#5262));
#953=EDGE_LOOP('',(#5263,#5264,#5265,#5266));
#954=EDGE_LOOP('',(#5267,#5268,#5269,#5270));
#955=EDGE_LOOP('',(#5271,#5272,#5273,#5274));
#956=EDGE_LOOP('',(#5275,#5276,#5277,#5278));
#957=EDGE_LOOP('',(#5279,#5280,#5281,#5282));
#958=EDGE_LOOP('',(#5283,#5284,#5285,#5286));
#959=EDGE_LOOP('',(#5287,#5288,#5289,#5290));
#960=EDGE_LOOP('',(#5291,#5292,#5293,#5294));
#961=EDGE_LOOP('',(#5295,#5296,#5297,#5298));
#962=EDGE_LOOP('',(#5299,#5300,#5301,#5302));
#963=EDGE_LOOP('',(#5303,#5304,#5305,#5306));
#964=EDGE_LOOP('',(#5307,#5308,#5309,#5310));
#965=EDGE_LOOP('',(#5311,#5312,#5313,#5314));
#966=EDGE_LOOP('',(#5315,#5316,#5317,#5318));
#967=EDGE_LOOP('',(#5319,#5320,#5321,#5322));
#968=EDGE_LOOP('',(#5323,#5324,#5325,#5326));
#969=EDGE_LOOP('',(#5327,#5328,#5329,#5330));
#970=EDGE_LOOP('',(#5331,#5332,#5333,#5334));
#971=EDGE_LOOP('',(#5335,#5336,#5337,#5338,#5339,#5340,#5341,#5342));
#972=EDGE_LOOP('',(#5343,#5344,#5345,#5346,#5347,#5348,#5349,#5350,#5351,
#5352,#5353,#5354,#5355,#5356,#5357,#5358,#5359,#5360,#5361,#5362,#5363,
#5364,#5365,#5366));
#973=EDGE_LOOP('',(#5367,#5368,#5369,#5370));
#974=EDGE_LOOP('',(#5371,#5372,#5373,#5374,#5375,#5376,#5377,#5378,#5379,
#5380,#5381,#5382,#5383,#5384,#5385,#5386,#5387,#5388,#5389,#5390,#5391,
#5392,#5393,#5394,#5395));
#975=EDGE_LOOP('',(#5396,#5397,#5398,#5399));
#976=EDGE_LOOP('',(#5400,#5401,#5402,#5403));
#977=EDGE_LOOP('',(#5404,#5405,#5406,#5407));
#978=EDGE_LOOP('',(#5408,#5409,#5410,#5411));
#979=EDGE_LOOP('',(#5412,#5413,#5414,#5415));
#980=EDGE_LOOP('',(#5416,#5417,#5418,#5419));
#981=EDGE_LOOP('',(#5420,#5421,#5422,#5423));
#982=EDGE_LOOP('',(#5424,#5425,#5426,#5427,#5428,#5429));
#983=EDGE_LOOP('',(#5430));
#984=EDGE_LOOP('',(#5431,#5432,#5433,#5434));
#985=EDGE_LOOP('',(#5435,#5436,#5437,#5438));
#986=EDGE_LOOP('',(#5439));
#987=EDGE_LOOP('',(#5440,#5441,#5442,#5443,#5444,#5445));
#988=EDGE_LOOP('',(#5446));
#1140=CIRCLE('',#6824,1.954);
#1141=CIRCLE('',#6835,1.5555);
#1142=CIRCLE('',#6846,1.954);
#1143=CIRCLE('',#6847,1.);
#1144=CIRCLE('',#6849,1.5555);
#1145=CIRCLE('',#6859,3.5);
#1146=CIRCLE('',#6861,3.5);
#1383=B_SPLINE_CURVE_WITH_KNOTS('',3,(#16353,#16354,#16355,#16356,#16357,
#16358,#16359,#16360,#16361,#16362),.UNSPECIFIED.,.F.,.F.,(4,3,3,4),(-4.09254174883832,
-3.98935377563313,-2.99201533172485,-2.06514013327812),.UNSPECIFIED.);
#1384=B_SPLINE_CURVE_WITH_KNOTS('',3,(#16365,#16366,#16367,#16368,#16369,
#16370,#16371),.UNSPECIFIED.,.F.,.F.,(4,3,4),(0.,0.998359650364244,1.11419103802955),
 .UNSPECIFIED.);
#1385=B_SPLINE_CURVE_WITH_KNOTS('',3,(#16376,#16377,#16378,#16379,#16380,
#16381,#16382,#16383,#16384,#16385,#16386,#16387,#16388,#16389,#16390,#16391,
#16392,#16393,#16394,#16395,#16396,#16397),.UNSPECIFIED.,.F.,.F.,(4,3,3,
3,3,3,3,4),(-10.3757270560179,-9.97338443908282,-8.97604599517454,-7.97870755126626,
-6.98136910735798,-5.98403066344969,-4.98669221954141,-4.09254174883832),
 .UNSPECIFIED.);
#1386=B_SPLINE_CURVE_WITH_KNOTS('',3,(#16398,#16399,#16400,#16401,#16402,
#16403,#16404,#16405,#16406,#16407,#16408,#16409,#16410,#16411,#16412,#16413,
#16414,#16415,#16416,#16417,#16418,#16419),.UNSPECIFIED.,.F.,.F.,(4,3,3,
3,3,3,3,4),(1.11419103802955,1.99671930072849,2.99507895109274,3.99343860145699,
4.99179825182123,5.99015790218548,6.98851755254973,7.39737634520914),
 .UNSPECIFIED.);
#1387=B_SPLINE_CURVE_WITH_KNOTS('',3,(#16424,#16425,#16426,#16427,#16428,
#16429,#16430,#16431,#16432,#16433,#16434,#16435,#16436,#16437,#16438,#16439,
#16440,#16441,#16442,#16443,#16444,#16445),.UNSPECIFIED.,.F.,.F.,(4,3,3,
3,3,3,3,4),(-16.6589123631975,-15.9574151025325,-14.9600766586242,-13.962738214716,
-12.9653997708077,-11.9680613268994,-10.9707228829911,-10.3757270560179),
 .UNSPECIFIED.);
#1388=B_SPLINE_CURVE_WITH_KNOTS('',3,(#16446,#16447,#16448,#16449,#16450,
#16451,#16452,#16453,#16454,#16455,#16456,#16457,#16458,#16459,#16460,#16461,
#16462,#16463,#16464,#16465,#16466,#16467),.UNSPECIFIED.,.F.,.F.,(4,3,3,
3,3,3,3,4),(7.39737634520914,7.98687720291397,8.98523685327822,9.98359650364247,
10.9819561540067,11.980315804371,12.9786754547352,13.6805616523887),
 .UNSPECIFIED.);
#1389=B_SPLINE_CURVE_WITH_KNOTS('',3,(#16472,#16473,#16474,#16475,#16476,
#16477,#16478,#16479,#16480,#16481,#16482,#16483,#16484,#16485,#16486,#16487,
#16488,#16489,#16490,#16491,#16492,#16493,#16494,#16495,#16496),
 .UNSPECIFIED.,.F.,.F.,(4,3,3,3,3,3,3,3,4),(-22.9420976703771,-22.9387842098905,
-21.9414457659822,-20.9441073220739,-19.9467688781656,-18.9494304342574,
-17.9520919903491,-16.9547535464408,-16.6589123631975),.UNSPECIFIED.);
#1390=B_SPLINE_CURVE_WITH_KNOTS('',3,(#16497,#16498,#16499,#16500,#16501,
#16502,#16503,#16504,#16505,#16506,#16507,#16508,#16509,#16510,#16511,#16512,
#16513,#16514,#16515,#16516,#16517,#16518),.UNSPECIFIED.,.F.,.F.,(4,3,3,
3,3,3,3,4),(13.6805616523887,13.9770351050995,14.9753947554637,15.973754405828,
16.9721140561922,17.9704737065565,18.9688333569207,19.9637469595683),
 .UNSPECIFIED.);
#1391=B_SPLINE_CURVE_WITH_KNOTS('',3,(#16523,#16524,#16525,#16526,#16527,
#16528,#16529,#16530,#16531,#16532,#16533,#16534,#16535,#16536,#16537,#16538,
#16539,#16540,#16541,#16542,#16543,#16544),.UNSPECIFIED.,.F.,.F.,(4,3,3,
3,3,3,3,4),(-29.2252829775567,-28.9228148733402,-27.9254764294319,-26.9281379855236,
-25.9307995416153,-24.9334610977071,-23.9361226537988,-22.9420976703771),
 .UNSPECIFIED.);
#1392=B_SPLINE_CURVE_WITH_KNOTS('',3,(#16545,#16546,#16547,#16548,#16549,
#16550,#16551,#16552,#16553,#16554,#16555,#16556,#16557,#16558,#16559,#16560,
#16561,#16562,#16563,#16564,#16565,#16566,#16567,#16568,#16569),
 .UNSPECIFIED.,.F.,.F.,(4,3,3,3,3,3,3,3,4),(19.9637469595683,19.967193007285,
20.9655526576492,21.9639123080134,22.9622719583777,23.9606316087419,24.9589912591062,
25.9573509094704,26.2469322667479),.UNSPECIFIED.);
#1393=B_SPLINE_CURVE_WITH_KNOTS('',3,(#16574,#16575,#16576,#16577,#16578,
#16579,#16580,#16581,#16582,#16583,#16584,#16585,#16586,#16587,#16588,#16589,
#16590,#16591,#16592,#16593,#16594,#16595),.UNSPECIFIED.,.F.,.F.,(4,3,3,
3,3,3,3,4),(-35.5084682847363,-34.9068455367899,-33.9095070928816,-32.9121686489733,
-31.914830205065,-30.9174917611567,-29.9201533172485,-29.2252829775567),
 .UNSPECIFIED.);
#1394=B_SPLINE_CURVE_WITH_KNOTS('',3,(#16596,#16597,#16598,#16599,#16600,
#16601,#16602,#16603,#16604,#16605,#16606,#16607,#16608,#16609,#16610,#16611,
#16612,#16613,#16614,#16615,#16616,#16617),.UNSPECIFIED.,.F.,.F.,(4,3,3,
3,3,3,3,4),(26.2469322667479,26.9557105598347,27.9540702101989,28.9524298605632,
29.9507895109274,30.9491491612917,31.9475088116559,32.5301175739275),
 .UNSPECIFIED.);
#1395=B_SPLINE_CURVE_WITH_KNOTS('',3,(#16622,#16623,#16624,#16625,#16626,
#16627,#16628,#16629,#16630,#16631,#16632,#16633,#16634,#16635,#16636,#16637,
#16638,#16639,#16640,#16641,#16642,#16643),.UNSPECIFIED.,.F.,.F.,(4,3,3,
3,3,3,3,4),(-41.7916535919158,-40.8908762002396,-39.8935377563313,-38.896199312423,
-37.8988608685147,-36.9015224246064,-35.9041839806982,-35.5084682847363),
 .UNSPECIFIED.);
#1396=B_SPLINE_CURVE_WITH_KNOTS('',3,(#16644,#16645,#16646,#16647,#16648,
#16649,#16650,#16651,#16652,#16653,#16654,#16655,#16656,#16657,#16658,#16659,
#16660,#16661,#16662,#16663,#16664,#16665),.UNSPECIFIED.,.F.,.F.,(4,3,3,
3,3,3,3,4),(32.5301175739275,32.9458684620202,33.9442281123844,34.9425877627486,
35.9409474131129,36.9393070634771,37.9376667138414,38.8133028811071),
 .UNSPECIFIED.);
#1397=B_SPLINE_CURVE_WITH_KNOTS('',3,(#16670,#16671,#16672,#16673,#16674,
#16675,#16676,#16677,#16678,#16679,#16680,#16681,#16682,#16683,#16684,#16685,
#16686,#16687,#16688,#16689,#16690,#16691,#16692,#16693,#16694),
 .UNSPECIFIED.,.F.,.F.,(4,3,3,3,3,3,3,3,4),(-48.0748388990954,-47.8722453075976,
-46.8749068636893,-45.877568419781,-44.8802299758727,-43.8828915319644,
-42.8855530880561,-41.8882146441479,-41.7916535919158),.UNSPECIFIED.);
#1398=B_SPLINE_CURVE_WITH_KNOTS('',3,(#16695,#16696,#16697,#16698,#16699,
#16700,#16701,#16702,#16703,#16704,#16705,#16706,#16707,#16708,#16709,#16710,
#16711,#16712,#16713,#16714,#16715,#16716,#16717,#16718,#16719),
 .UNSPECIFIED.,.F.,.F.,(4,3,3,3,3,3,3,3,4),(38.8133028811071,38.9360263642056,
39.9343860145699,40.9327456649341,41.9311053152984,42.9294649656626,43.9278246160269,
44.9261842663911,45.0964881882867),.UNSPECIFIED.);
#1399=B_SPLINE_CURVE_WITH_KNOTS('',3,(#16724,#16725,#16726,#16727,#16728,
#16729,#16730,#16731,#16732,#16733,#16734,#16735,#16736,#16737,#16738,#16739,
#16740,#16741,#16742,#16743,#16744,#16745),.UNSPECIFIED.,.F.,.F.,(4,3,3,
3,3,3,3,4),(-54.358024206275,-53.8562759710472,-52.858937527139,-51.8615990832307,
-50.8642606393224,-49.8669221954141,-48.8695837515058,-48.0748388990954),
 .UNSPECIFIED.);
#1400=B_SPLINE_CURVE_WITH_KNOTS('',3,(#16746,#16747,#16748,#16749,#16750,
#16751,#16752,#16753,#16754,#16755,#16756,#16757,#16758,#16759,#16760,#16761,
#16762,#16763,#16764,#16765,#16766,#16767),.UNSPECIFIED.,.F.,.F.,(4,3,3,
3,3,3,3,4),(45.0964881882867,45.9245439167554,46.9229035671196,47.9212632174839,
48.9196228678481,49.9179825182124,50.9163421685766,51.3796734954663),
 .UNSPECIFIED.);
#1401=B_SPLINE_CURVE_WITH_KNOTS('',3,(#16772,#16773,#16774,#16775,#16776,
#16777,#16778,#16779,#16780,#16781,#16782,#16783,#16784,#16785,#16786,#16787,
#16788,#16789,#16790,#16791,#16792,#16793),.UNSPECIFIED.,.F.,.F.,(4,3,3,
3,3,3,3,4),(-60.6412095134546,-59.8403066344969,-58.8429681905886,-57.8456297466804,
-56.8482913027721,-55.8509528588638,-54.8536144149555,-54.358024206275),
 .UNSPECIFIED.);
#1402=B_SPLINE_CURVE_WITH_KNOTS('',3,(#16794,#16795,#16796,#16797,#16798,
#16799,#16800,#16801,#16802,#16803,#16804,#16805,#16806,#16807,#16808,#16809,
#16810,#16811,#16812,#16813,#16814,#16815),.UNSPECIFIED.,.F.,.F.,(4,3,3,
3,3,3,3,4),(51.3796734954663,51.9147018189409,52.9130614693051,53.9114211196693,
54.9097807700336,55.9081404203978,56.9065000707621,57.6628588026459),
 .UNSPECIFIED.);
#1403=B_SPLINE_CURVE_WITH_KNOTS('',3,(#16821,#16822,#16823,#16824,#16825,
#16826,#16827,#16828,#16829,#16830),.UNSPECIFIED.,.F.,.F.,(4,1,1,1,1,1,
1,4),(72.2566310325653,72.4530665975158,73.4504050414241,74.4477434853324,
75.4450819292407,76.4424203731489,77.4397588170572,78.4370972609655),
 .UNSPECIFIED.);
#1404=B_SPLINE_CURVE_WITH_KNOTS('',3,(#16833,#16834,#16835,#16836,#16837,
#16838,#16839,#16840),.UNSPECIFIED.,.F.,.F.,(4,1,1,1,1,4),(72.2566310325652,
73.2039641964158,74.2023238467801,75.2006834971443,76.1990431475085,77.1974027978728),
 .UNSPECIFIED.);
#1405=B_SPLINE_CURVE_WITH_KNOTS('',3,(#16845,#16846,#16847,#16848,#16849,
#16850,#16851,#16852,#16853,#16854),.UNSPECIFIED.,.F.,.F.,(4,1,1,1,1,1,
1,4),(65.9734457253856,66.4690359340661,67.4663743779744,68.4637128218827,
69.461051265791,70.4583897096992,71.4557281536075,72.2566310325653),
 .UNSPECIFIED.);
#1406=B_SPLINE_CURVE_WITH_KNOTS('',3,(#16855,#16856,#16857,#16858,#16859,
#16860,#16861,#16862,#16863,#16864,#16865),.UNSPECIFIED.,.F.,.F.,(4,1,1,
1,1,1,1,1,4),(65.9734457253856,66.2154466438661,67.2138062942303,68.2121659445946,
69.2105255949588,70.2088852453231,71.2072448956873,72.2056045460516,72.2566310325652),
 .UNSPECIFIED.);
#1407=B_SPLINE_CURVE_WITH_KNOTS('',3,(#16870,#16871,#16872,#16873,#16874,
#16875,#16876,#16877,#16878,#16879),.UNSPECIFIED.,.F.,.F.,(4,1,1,1,1,1,
1,4),(59.6902604182061,60.4850052706164,61.4823437145247,62.479682158433,
63.4770206023413,64.4743590462496,65.4716974901578,65.9734457253856),
 .UNSPECIFIED.);
#1408=B_SPLINE_CURVE_WITH_KNOTS('',3,(#16880,#16881,#16882,#16883,#16884,
#16885,#16886,#16887,#16888,#16889),.UNSPECIFIED.,.F.,.F.,(4,1,1,1,1,1,
1,4),(59.6902604182061,60.2252887416806,61.2236483920448,62.2220080424091,
63.2203676927733,64.2187273431376,65.2170869935018,65.9734457253856),
 .UNSPECIFIED.);
#1409=B_SPLINE_CURVE_WITH_KNOTS('',3,(#16894,#16895,#16896,#16897,#16898,
#16899,#16900,#16901,#16902,#16903,#16904),.UNSPECIFIED.,.F.,.F.,(4,1,1,
1,1,1,1,1,4),(53.4070751110265,53.5036361632585,54.5009746071667,55.498313051075,
56.4956514949833,57.4929899388916,58.4903283827999,59.4876668267081,59.6902604182061),
 .UNSPECIFIED.);
#1410=B_SPLINE_CURVE_WITH_KNOTS('',3,(#16905,#16906,#16907,#16908,#16909,
#16910,#16911,#16912,#16913,#16914),.UNSPECIFIED.,.F.,.F.,(4,1,1,1,1,1,
1,4),(53.4070751110265,54.2351308394951,55.2334904898594,56.2318501402236,
57.2302097905879,58.2285694409521,59.2269290913164,59.6902604182061),
 .UNSPECIFIED.);
#1411=B_SPLINE_CURVE_WITH_KNOTS('',3,(#16919,#16920,#16921,#16922,#16923,
#16924,#16925,#16926,#16927,#16928),.UNSPECIFIED.,.F.,.F.,(4,1,1,1,1,1,
1,4),(47.1238898038469,47.5196054998088,48.516943943717,49.5142823876253,
50.5116208315336,51.5089592754419,52.5062977193502,53.4070751110265),
 .UNSPECIFIED.);
#1412=B_SPLINE_CURVE_WITH_KNOTS('',3,(#16929,#16930,#16931,#16932,#16933,
#16934,#16935,#16936,#16937,#16938,#16939),.UNSPECIFIED.,.F.,.F.,(4,1,1,
1,1,1,1,1,4),(47.1238898038469,47.2466132869454,48.2449729373096,49.2433325876739,
50.2416922380381,51.2400518884024,52.2384115387666,53.2367711891309,53.4070751110265),
 .UNSPECIFIED.);
#1413=B_SPLINE_CURVE_WITH_KNOTS('',3,(#16944,#16945,#16946,#16947,#16948,
#16949,#16950,#16951,#16952,#16953),.UNSPECIFIED.,.F.,.F.,(4,1,1,1,1,1,
1,4),(40.8407044966673,41.5355748363591,42.5329132802674,43.5302517241756,
44.5275901680839,45.5249286119922,46.5222670559005,47.1238898038469),
 .UNSPECIFIED.);
#1414=B_SPLINE_CURVE_WITH_KNOTS('',3,(#16954,#16955,#16956,#16957,#16958,
#16959,#16960,#16961,#16962,#16963),.UNSPECIFIED.,.F.,.F.,(4,1,1,1,1,1,
1,4),(40.8407044966673,41.2564553847599,42.2548150351241,43.2531746854884,
44.2515343358526,45.2498939862169,46.2482536365811,47.1238898038469),
 .UNSPECIFIED.);
#1415=B_SPLINE_CURVE_WITH_KNOTS('',3,(#16968,#16969,#16970,#16971,#16972,
#16973,#16974,#16975,#16976,#16977),.UNSPECIFIED.,.F.,.F.,(4,1,1,1,1,1,
1,4),(34.5575191894877,35.5515441729094,36.5488826168177,37.5462210607259,
38.5435595046342,39.5408979485425,40.5382363924508,40.8407044966673),
 .UNSPECIFIED.);
#1416=B_SPLINE_CURVE_WITH_KNOTS('',3,(#16978,#16979,#16980,#16981,#16982,
#16983,#16984,#16985,#16986,#16987),.UNSPECIFIED.,.F.,.F.,(4,1,1,1,1,1,
1,4),(34.5575191894877,35.2662974825744,36.2646571329387,37.2630167833029,
38.2613764336672,39.2597360840314,40.2580957343957,40.8407044966673),
 .UNSPECIFIED.);
#1417=B_SPLINE_CURVE_WITH_KNOTS('',3,(#16992,#16993,#16994,#16995,#16996,
#16997,#16998,#16999,#17000,#17001,#17002),.UNSPECIFIED.,.F.,.F.,(4,1,1,
1,1,1,1,1,4),(28.2743338823081,28.5701750655514,29.5675135094597,30.564851953368,
31.5621903972762,32.5595288411845,33.5568672850928,34.5542057290011,34.5575191894877),
 .UNSPECIFIED.);
#1418=B_SPLINE_CURVE_WITH_KNOTS('',3,(#17003,#17004,#17005,#17006,#17007,
#17008,#17009,#17010,#17011,#17012,#17013),.UNSPECIFIED.,.F.,.F.,(4,1,1,
1,1,1,1,1,4),(28.2743338823081,28.2777799300247,29.2761395803889,30.2744992307532,
31.2728588811174,32.2712185314817,33.2695781818459,34.2679378322102,34.5575191894877),
 .UNSPECIFIED.);
#1419=B_SPLINE_CURVE_WITH_KNOTS('',3,(#17018,#17019,#17020,#17021,#17022,
#17023,#17024,#17025,#17026,#17027),.UNSPECIFIED.,.F.,.F.,(4,1,1,1,1,1,
1,4),(21.9911485751285,22.5861444021017,23.58348284601,24.5808212899183,
25.5781597338266,26.5754981777348,27.5728366216431,28.2743338823081),
 .UNSPECIFIED.);
#1420=B_SPLINE_CURVE_WITH_KNOTS('',3,(#17028,#17029,#17030,#17031,#17032,
#17033,#17034,#17035,#17036,#17037),.UNSPECIFIED.,.F.,.F.,(4,1,1,1,1,1,
1,4),(21.9911485751285,22.2876220278392,23.2859816782034,24.2843413285677,
25.2827009789319,26.2810606292962,27.2794202796604,28.2743338823081),
 .UNSPECIFIED.);
#1421=B_SPLINE_CURVE_WITH_KNOTS('',3,(#17042,#17043,#17044,#17045,#17046,
#17047,#17048,#17049,#17050,#17051),.UNSPECIFIED.,.F.,.F.,(4,1,1,1,1,1,
1,4),(15.7079632679489,16.602113738652,17.5994521825603,18.5967906264686,
19.5941290703769,20.5914675142851,21.5888059581934,21.9911485751285),
 .UNSPECIFIED.);
#1422=B_SPLINE_CURVE_WITH_KNOTS('',3,(#17052,#17053,#17054,#17055,#17056,
#17057,#17058,#17059,#17060,#17061),.UNSPECIFIED.,.F.,.F.,(4,1,1,1,1,1,
1,4),(15.7079632679489,16.2974641256537,17.295823776018,18.2941834263822,
19.2925430767465,20.2909027271107,21.289262377475,21.9911485751285),
 .UNSPECIFIED.);
#1423=B_SPLINE_CURVE_WITH_KNOTS('',3,(#17064,#17065,#17066,#17067,#17068,
#17069,#17070,#17071,#17072,#17073,#17074,#17075,#17076,#17077,#17078,#17079,
#17080,#17081,#17082,#17083,#17084,#17085,#17086,#17087,#17088,#17089,#17090,
#17091,#17092,#17093,#17094,#17095,#17096,#17097,#17098,#17099,#17100,#17101,
#17102,#17103,#17104,#17105,#17106,#17107,#17108,#17109,#17110,#17111,#17112,
#17113,#17114,#17115,#17116,#17117,#17118,#17119,#17120,#17121,#17122,#17123,
#17124,#17125,#17126,#17127,#17128,#17129,#17130,#17131,#17132,#17133,#17134,
#17135,#17136,#17137,#17138,#17139,#17140,#17141,#17142,#17143,#17144,#17145,
#17146,#17147,#17148,#17149,#17150,#17151,#17152,#17153,#17154,#17155,#17156,
#17157,#17158,#17159,#17160,#17161,#17162,#17163,#17164,#17165,#17166,#17167,
#17168,#17169,#17170,#17171,#17172,#17173,#17174,#17175,#17176,#17177,#17178,
#17179,#17180,#17181,#17182,#17183,#17184,#17185,#17186,#17187,#17188,#17189,
#17190,#17191,#17192,#17193,#17194,#17195,#17196,#17197,#17198,#17199,#17200,
#17201,#17202,#17203,#17204,#17205,#17206,#17207,#17208,#17209,#17210,#17211,
#17212,#17213,#17214,#17215,#17216,#17217,#17218,#17219,#17220,#17221,#17222,
#17223,#17224,#17225,#17226,#17227,#17228,#17229,#17230,#17231,#17232,#17233,
#17234,#17235,#17236,#17237,#17238,#17239,#17240,#17241,#17242,#17243,#17244,
#17245,#17246,#17247,#17248,#17249,#17250,#17251,#17252,#17253,#17254,#17255,
#17256,#17257,#17258,#17259,#17260,#17261,#17262,#17263,#17264,#17265,#17266,
#17267,#17268),.UNSPECIFIED.,.F.,.F.,(4,3,3,3,3,3,3,3,3,3,3,3,3,3,3,3,3,
3,3,3,3,3,3,3,3,3,3,3,3,3,3,3,3,3,3,3,3,3,3,3,3,3,3,3,3,3,3,3,3,3,3,3,3,
3,3,3,3,3,3,3,3,3,3,3,3,3,3,3,4),(-0.996917990983889,-0.978871820698626,
-0.961104366684017,-0.951552920986235,-0.947856438601261,-0.928927311919591,
-0.909844934708151,-0.904827747876617,-0.901690020918146,-0.882383426909664,
-0.863197144412726,-0.849964666497242,-0.841946217765742,-0.838653066670214,
-0.836732188581758,-0.818195847210497,-0.79884286378821,-0.782668226932182,
-0.778162385717433,-0.774287931072979,-0.754720517493441,-0.734912656248282,
-0.718545934421209,-0.712508687338266,-0.709097549624951,-0.689177599037007,
-0.66944576893999,-0.649768871196005,-0.645300371314176,-0.641533261094732,
-0.621745212512907,-0.601563770435519,-0.588280416256018,-0.579851467607475,
-0.575105400436484,-0.55460765219522,-0.534203727151442,-0.514750332075477,
-0.510181591792683,-0.506682086087755,-0.495296936999511,-0.475415657124971,
-0.455258237398922,-0.446439366268775,-0.440745412953617,-0.437134753004049,
-0.41645257608894,-0.395479514073081,-0.375148710383956,-0.368821709024976,
-0.365366889657485,-0.344172462410384,-0.323356461419818,-0.31415629931658,
-0.303019600034791,-0.297245219492413,-0.293778204123757,-0.272935156968737,
-0.251638706464901,-0.237180007007782,-0.228159672465448,-0.224715742096491,
-0.221072456791868,-0.199410898099475,-0.17780203126093,-0.156885571034439,
-0.151911241963545,-0.148372189075213,-0.135969110807948),.UNSPECIFIED.);
#1424=B_SPLINE_CURVE_WITH_KNOTS('',3,(#17270,#17271,#17272,#17273,#17274,
#17275,#17276,#17277,#17278,#17279,#17280,#17281,#17282,#17283,#17284,#17285,
#17286,#17287,#17288,#17289,#17290,#17291,#17292,#17293,#17294,#17295,#17296,
#17297,#17298,#17299,#17300,#17301,#17302,#17303,#17304,#17305,#17306,#17307,
#17308,#17309,#17310,#17311,#17312,#17313,#17314,#17315,#17316,#17317,#17318,
#17319,#17320,#17321,#17322,#17323,#17324,#17325,#17326,#17327),
 .UNSPECIFIED.,.F.,.F.,(4,3,3,3,3,3,3,3,3,3,3,3,3,3,3,3,3,3,3,4),(-0.271362855059846,
-0.249815149227379,-0.228817911637578,-0.214757147690894,-0.202696405081427,
-0.199258885355278,-0.179079500439592,-0.172574855850844,-0.151002998869488,
-0.132127624010802,-0.128545226638174,-0.108660379749781,-0.0889046558653028,
-0.0695674270863146,-0.0643977980835871,-0.0611874131352371,-0.042433397437552,
-0.0240016538661123,-0.00610725636958426,0.),.UNSPECIFIED.);
#1425=B_SPLINE_CURVE_WITH_KNOTS('',3,(#17330,#17331,#17332,#17333,#17334,
#17335,#17336,#17337,#17338,#17339,#17340,#17341,#17342,#17343,#17344,#17345,
#17346,#17347,#17348,#17349,#17350,#17351,#17352,#17353,#17354,#17355,#17356,
#17357),.UNSPECIFIED.,.F.,.F.,(4,3,3,3,3,3,3,3,3,4),(-0.135969110807948,
-0.126188073854222,-0.104892740575823,-0.0831670570417323,-0.0779384685470277,
-0.0734086019617295,-0.0516285578143609,-0.0295399653803274,-0.00752416693119264,
0.),.UNSPECIFIED.);
#1426=B_SPLINE_CURVE_WITH_KNOTS('',3,(#17642,#17643,#17644,#17645,#17646,
#17647,#17648,#17649),.UNSPECIFIED.,.F.,.F.,(4,1,1,1,1,4),(11.6154215191106,
12.6127599630189,13.6100984069272,14.6074368508354,15.6047752947437,15.7079632679489),
 .UNSPECIFIED.);
#1427=B_SPLINE_CURVE_WITH_KNOTS('',3,(#17650,#17651,#17652,#17653,#17654,
#17655,#17656,#17657,#17658,#17659,#17660,#17661,#17662,#17663,#17664,#17665,
#17666,#17667,#17668,#17669,#17670,#17671,#17672,#17673,#17674,#17675,#17676,
#17677,#17678,#17679,#17680,#17681,#17682,#17683,#17684,#17685,#17686,#17687,
#17688,#17689,#17690,#17691,#17692,#17693,#17694,#17695,#17696,#17697,#17698,
#17699,#17700,#17701,#17702,#17703,#17704,#17705,#17706,#17707,#17708,#17709,
#17710,#17711,#17712,#17713,#17714,#17715,#17716,#17717,#17718,#17719,#17720,
#17721,#17722,#17723,#17724,#17725,#17726,#17727,#17728,#17729,#17730,#17731,
#17732,#17733,#17734),.UNSPECIFIED.,.F.,.F.,(4,3,3,3,3,3,3,3,3,3,3,3,3,
3,3,3,3,3,3,3,3,3,3,3,3,3,3,3,4),(-0.364629307890661,-0.350886771084415,
-0.329297510939725,-0.318979842765136,-0.313748856729508,-0.309367238941102,
-0.288044972781349,-0.272811108278258,-0.264009728102714,-0.260298972601032,
-0.239567880035138,-0.219347617431434,-0.206054227262732,-0.194878207820902,
-0.191399429390758,-0.17181371271556,-0.166174056756627,-0.145402299662048,
-0.12670765132229,-0.123381127587156,-0.103926762733045,-0.0845494608218094,
-0.0655688723802368,-0.0621691825638593,-0.0589309125894093,-0.0403408647045067,
-0.0220852216194749,-0.00441218938162483,0.),.UNSPECIFIED.);
#1428=B_SPLINE_CURVE_WITH_KNOTS('',3,(#17735,#17736,#17737,#17738,#17739,
#17740,#17741,#17742,#17743,#17744,#17745,#17746,#17747,#17748,#17749,#17750,
#17751,#17752,#17753),.UNSPECIFIED.,.F.,.F.,(4,3,3,3,3,3,4),(-65.3098882395457,
-64.8269988540384,-63.8296604101301,-62.8323219662218,-61.8349835223135,
-60.8376450784052,-60.6412095134546),.UNSPECIFIED.);
#1429=B_SPLINE_CURVE_WITH_KNOTS('',3,(#17756,#17757,#17758,#17759,#17760,
#17761,#17762,#17763,#17764),.UNSPECIFIED.,.F.,.F.,(4,1,1,1,1,1,4),(10.3757270560179,
11.3056658738325,12.3040255241967,13.302385174561,14.3007448249252,15.2991044752895,
15.7079632679489),.UNSPECIFIED.);
#1430=B_SPLINE_CURVE_WITH_KNOTS('',3,(#18054,#18055,#18056,#18057,#18058,
#18059,#18060,#18061,#18062,#18063,#18064,#18065,#18066,#18067,#18068,#18069,
#18070,#18071,#18072,#18073,#18074,#18075),.UNSPECIFIED.,.F.,.F.,(4,3,3,
3,3,3,3,4),(57.6628588026459,57.9048597211263,58.9032193714906,59.9015790218548,
60.8999386722191,61.8982983225833,62.8966579729476,63.2447481062677),
 .UNSPECIFIED.);
#1431=B_SPLINE_CURVE_WITH_KNOTS('',3,(#18076,#18077,#18078,#18079,#18080,
#18081,#18082,#18083,#18084,#18085,#18086,#18087,#18088,#18089,#18090,#18091,
#18092,#18093,#18094,#18095,#18096,#18097,#18098,#18099,#18100,#18101,#18102,
#18103,#18104,#18105,#18106,#18107,#18108,#18109,#18110,#18111,#18112,#18113,
#18114,#18115,#18116,#18117,#18118,#18119,#18120,#18121,#18122,#18123,#18124,
#18125,#18126,#18127,#18128,#18129,#18130,#18131,#18132,#18133,#18134,#18135,
#18136,#18137,#18138,#18139,#18140,#18141,#18142,#18143,#18144,#18145,#18146,
#18147,#18148,#18149,#18150,#18151,#18152,#18153,#18154,#18155,#18156,#18157),
 .UNSPECIFIED.,.F.,.F.,(4,3,3,3,3,3,3,3,3,3,3,3,3,3,3,3,3,3,3,3,3,3,3,3,
3,3,3,4),(-0.366397579005847,-0.355573362530754,-0.337605442405704,-0.327398200425482,
-0.321620335202968,-0.30281021010297,-0.288367976755365,-0.281197910953663,
-0.277581602535663,-0.258139779174731,-0.23832225991534,-0.225559780767037,
-0.21845666374658,-0.214865898441521,-0.194435927724086,-0.187272343322128,
-0.167568574984456,-0.146399230996079,-0.142991450501546,-0.122489503287978,
-0.101565610408655,-0.0804999660718792,-0.0757146540182571,-0.0722132271210984,
-0.0505693460362938,-0.0288755213118303,-0.00764564704115539,0.),
 .UNSPECIFIED.);
#1865=LINE('',#16351,#2321);
#1866=LINE('',#16375,#2322);
#1867=LINE('',#16423,#2323);
#1868=LINE('',#16471,#2324);
#1869=LINE('',#16522,#2325);
#1870=LINE('',#16573,#2326);
#1871=LINE('',#16621,#2327);
#1872=LINE('',#16669,#2328);
#1873=LINE('',#16723,#2329);
#1874=LINE('',#16771,#2330);
#1875=LINE('',#16819,#2331);
#1876=LINE('',#16844,#2332);
#1877=LINE('',#16869,#2333);
#1878=LINE('',#16893,#2334);
#1879=LINE('',#16918,#2335);
#1880=LINE('',#16943,#2336);
#1881=LINE('',#16967,#2337);
#1882=LINE('',#16991,#2338);
#1883=LINE('',#17017,#2339);
#1884=LINE('',#17041,#2340);
#1885=LINE('',#17359,#2341);
#1886=LINE('',#18162,#2342);
#1887=LINE('',#18164,#2343);
#1888=LINE('',#18166,#2344);
#1889=LINE('',#18167,#2345);
#1890=LINE('',#18170,#2346);
#1891=LINE('',#18172,#2347);
#1892=LINE('',#18173,#2348);
#1893=LINE('',#18176,#2349);
#1894=LINE('',#18178,#2350);
#1895=LINE('',#18179,#2351);
#1896=LINE('',#18182,#2352);
#1897=LINE('',#18184,#2353);
#1898=LINE('',#18185,#2354);
#1899=LINE('',#18188,#2355);
#1900=LINE('',#18190,#2356);
#1901=LINE('',#18191,#2357);
#1902=LINE('',#18193,#2358);
#1903=LINE('',#18194,#2359);
#1904=LINE('',#18201,#2360);
#2321=VECTOR('',#7947,2.);
#2322=VECTOR('',#7952,2.);
#2323=VECTOR('',#7955,2.);
#2324=VECTOR('',#7958,2.);
#2325=VECTOR('',#7961,2.);
#2326=VECTOR('',#7964,2.);
#2327=VECTOR('',#7967,2.);
#2328=VECTOR('',#7970,2.);
#2329=VECTOR('',#7973,2.);
#2330=VECTOR('',#7976,2.);
#2331=VECTOR('',#7979,1.5555);
#2332=VECTOR('',#7984,1.5555);
#2333=VECTOR('',#7987,1.5555);
#2334=VECTOR('',#7990,1.5555);
#2335=VECTOR('',#7993,1.5555);
#2336=VECTOR('',#7996,1.5555);
#2337=VECTOR('',#7999,1.5555);
#2338=VECTOR('',#8002,1.5555);
#2339=VECTOR('',#8005,1.5555);
#2340=VECTOR('',#8008,1.5555);
#2341=VECTOR('',#8013,1.5);
#2342=VECTOR('',#8024,10.);
#2343=VECTOR('',#8025,10.);
#2344=VECTOR('',#8026,10.);
#2345=VECTOR('',#8027,10.);
#2346=VECTOR('',#8030,10.);
#2347=VECTOR('',#8031,10.);
#2348=VECTOR('',#8032,10.);
#2349=VECTOR('',#8035,10.);
#2350=VECTOR('',#8036,10.);
#2351=VECTOR('',#8037,10.);
#2352=VECTOR('',#8040,10.);
#2353=VECTOR('',#8041,10.);
#2354=VECTOR('',#8042,10.);
#2355=VECTOR('',#8045,10.);
#2356=VECTOR('',#8046,10.);
#2357=VECTOR('',#8047,10.);
#2358=VECTOR('',#8050,10.);
#2359=VECTOR('',#8051,10.);
#2360=VECTOR('',#8060,3.5);
#2855=VERTEX_POINT('',#16349);
#2856=VERTEX_POINT('',#16350);
#2857=VERTEX_POINT('',#16352);
#2858=VERTEX_POINT('',#16363);
#2859=VERTEX_POINT('',#16373);
#2860=VERTEX_POINT('',#16374);
#2861=VERTEX_POINT('',#16421);
#2862=VERTEX_POINT('',#16422);
#2863=VERTEX_POINT('',#16469);
#2864=VERTEX_POINT('',#16470);
#2865=VERTEX_POINT('',#16520);
#2866=VERTEX_POINT('',#16521);
#2867=VERTEX_POINT('',#16571);
#2868=VERTEX_POINT('',#16572);
#2869=VERTEX_POINT('',#16619);
#2870=VERTEX_POINT('',#16620);
#2871=VERTEX_POINT('',#16667);
#2872=VERTEX_POINT('',#16668);
#2873=VERTEX_POINT('',#16721);
#2874=VERTEX_POINT('',#16722);
#2875=VERTEX_POINT('',#16769);
#2876=VERTEX_POINT('',#16770);
#2877=VERTEX_POINT('',#16817);
#2878=VERTEX_POINT('',#16818);
#2879=VERTEX_POINT('',#16820);
#2880=VERTEX_POINT('',#16831);
#2881=VERTEX_POINT('',#16842);
#2882=VERTEX_POINT('',#16843);
#2883=VERTEX_POINT('',#16867);
#2884=VERTEX_POINT('',#16868);
#2885=VERTEX_POINT('',#16891);
#2886=VERTEX_POINT('',#16892);
#2887=VERTEX_POINT('',#16916);
#2888=VERTEX_POINT('',#16917);
#2889=VERTEX_POINT('',#16941);
#2890=VERTEX_POINT('',#16942);
#2891=VERTEX_POINT('',#16965);
#2892=VERTEX_POINT('',#16966);
#2893=VERTEX_POINT('',#16989);
#2894=VERTEX_POINT('',#16990);
#2895=VERTEX_POINT('',#17015);
#2896=VERTEX_POINT('',#17016);
#2897=VERTEX_POINT('',#17039);
#2898=VERTEX_POINT('',#17040);
#2899=VERTEX_POINT('',#17063);
#2900=VERTEX_POINT('',#17269);
#2901=VERTEX_POINT('',#17328);
#2902=VERTEX_POINT('',#17358);
#2903=VERTEX_POINT('',#17641);
#2904=VERTEX_POINT('',#17755);
#2905=VERTEX_POINT('',#18160);
#2906=VERTEX_POINT('',#18161);
#2907=VERTEX_POINT('',#18163);
#2908=VERTEX_POINT('',#18165);
#2909=VERTEX_POINT('',#18169);
#2910=VERTEX_POINT('',#18171);
#2911=VERTEX_POINT('',#18175);
#2912=VERTEX_POINT('',#18177);
#2913=VERTEX_POINT('',#18181);
#2914=VERTEX_POINT('',#18183);
#2915=VERTEX_POINT('',#18187);
#2916=VERTEX_POINT('',#18189);
#2917=VERTEX_POINT('',#18197);
#2918=VERTEX_POINT('',#18200);
#3687=EDGE_CURVE('',#2855,#2856,#1865,.T.);
#3688=EDGE_CURVE('',#2855,#2857,#1383,.T.);
#3689=EDGE_CURVE('',#2857,#2858,#1140,.F.);
#3690=EDGE_CURVE('',#2858,#2856,#1384,.T.);
#3691=EDGE_CURVE('',#2859,#2860,#1866,.T.);
#3692=EDGE_CURVE('',#2859,#2855,#1385,.T.);
#3693=EDGE_CURVE('',#2856,#2860,#1386,.T.);
#3694=EDGE_CURVE('',#2861,#2862,#1867,.T.);
#3695=EDGE_CURVE('',#2861,#2859,#1387,.T.);
#3696=EDGE_CURVE('',#2860,#2862,#1388,.T.);
#3697=EDGE_CURVE('',#2863,#2864,#1868,.T.);
#3698=EDGE_CURVE('',#2863,#2861,#1389,.T.);
#3699=EDGE_CURVE('',#2862,#2864,#1390,.T.);
#3700=EDGE_CURVE('',#2865,#2866,#1869,.T.);
#3701=EDGE_CURVE('',#2865,#2863,#1391,.T.);
#3702=EDGE_CURVE('',#2864,#2866,#1392,.T.);
#3703=EDGE_CURVE('',#2867,#2868,#1870,.T.);
#3704=EDGE_CURVE('',#2867,#2865,#1393,.T.);
#3705=EDGE_CURVE('',#2866,#2868,#1394,.T.);
#3706=EDGE_CURVE('',#2869,#2870,#1871,.T.);
#3707=EDGE_CURVE('',#2869,#2867,#1395,.T.);
#3708=EDGE_CURVE('',#2868,#2870,#1396,.T.);
#3709=EDGE_CURVE('',#2871,#2872,#1872,.T.);
#3710=EDGE_CURVE('',#2871,#2869,#1397,.T.);
#3711=EDGE_CURVE('',#2870,#2872,#1398,.T.);
#3712=EDGE_CURVE('',#2873,#2874,#1873,.T.);
#3713=EDGE_CURVE('',#2873,#2871,#1399,.T.);
#3714=EDGE_CURVE('',#2872,#2874,#1400,.T.);
#3715=EDGE_CURVE('',#2875,#2876,#1874,.T.);
#3716=EDGE_CURVE('',#2875,#2873,#1401,.T.);
#3717=EDGE_CURVE('',#2874,#2876,#1402,.T.);
#3718=EDGE_CURVE('',#2877,#2878,#1875,.T.);
#3719=EDGE_CURVE('',#2877,#2879,#1403,.T.);
#3720=EDGE_CURVE('',#2879,#2880,#1141,.T.);
#3721=EDGE_CURVE('',#2878,#2880,#1404,.T.);
#3722=EDGE_CURVE('',#2881,#2882,#1876,.T.);
#3723=EDGE_CURVE('',#2881,#2877,#1405,.T.);
#3724=EDGE_CURVE('',#2882,#2878,#1406,.T.);
#3725=EDGE_CURVE('',#2883,#2884,#1877,.T.);
#3726=EDGE_CURVE('',#2883,#2881,#1407,.T.);
#3727=EDGE_CURVE('',#2884,#2882,#1408,.T.);
#3728=EDGE_CURVE('',#2885,#2886,#1878,.T.);
#3729=EDGE_CURVE('',#2885,#2883,#1409,.T.);
#3730=EDGE_CURVE('',#2886,#2884,#1410,.T.);
#3731=EDGE_CURVE('',#2887,#2888,#1879,.T.);
#3732=EDGE_CURVE('',#2887,#2885,#1411,.T.);
#3733=EDGE_CURVE('',#2888,#2886,#1412,.T.);
#3734=EDGE_CURVE('',#2889,#2890,#1880,.T.);
#3735=EDGE_CURVE('',#2889,#2887,#1413,.T.);
#3736=EDGE_CURVE('',#2890,#2888,#1414,.T.);
#3737=EDGE_CURVE('',#2891,#2892,#1881,.T.);
#3738=EDGE_CURVE('',#2891,#2889,#1415,.T.);
#3739=EDGE_CURVE('',#2892,#2890,#1416,.T.);
#3740=EDGE_CURVE('',#2893,#2894,#1882,.T.);
#3741=EDGE_CURVE('',#2893,#2891,#1417,.T.);
#3742=EDGE_CURVE('',#2894,#2892,#1418,.T.);
#3743=EDGE_CURVE('',#2895,#2896,#1883,.T.);
#3744=EDGE_CURVE('',#2895,#2893,#1419,.T.);
#3745=EDGE_CURVE('',#2896,#2894,#1420,.T.);
#3746=EDGE_CURVE('',#2897,#2898,#1884,.T.);
#3747=EDGE_CURVE('',#2897,#2895,#1421,.T.);
#3748=EDGE_CURVE('',#2898,#2896,#1422,.T.);
#3749=EDGE_CURVE('',#2880,#2899,#1423,.T.);
#3750=EDGE_CURVE('',#2900,#2879,#1424,.T.);
#3751=EDGE_CURVE('',#2901,#2900,#1142,.T.);
#3752=EDGE_CURVE('',#2899,#2901,#1425,.T.);
#3753=EDGE_CURVE('',#2899,#2902,#1885,.T.);
#3754=EDGE_CURVE('',#2902,#2902,#1143,.T.);
#3755=EDGE_CURVE('',#2903,#2897,#1426,.T.);
#3756=EDGE_CURVE('',#2857,#2903,#1427,.T.);
#3757=EDGE_CURVE('',#2900,#2875,#1428,.T.);
#3758=EDGE_CURVE('',#2904,#2898,#1429,.T.);
#3759=EDGE_CURVE('',#2903,#2904,#1144,.T.);
#3760=EDGE_CURVE('',#2876,#2901,#1430,.T.);
#3761=EDGE_CURVE('',#2904,#2858,#1431,.T.);
#3762=EDGE_CURVE('',#2905,#2906,#1886,.T.);
#3763=EDGE_CURVE('',#2905,#2907,#1887,.T.);
#3764=EDGE_CURVE('',#2907,#2908,#1888,.T.);
#3765=EDGE_CURVE('',#2906,#2908,#1889,.T.);
#3766=EDGE_CURVE('',#2909,#2905,#1890,.T.);
#3767=EDGE_CURVE('',#2909,#2910,#1891,.T.);
#3768=EDGE_CURVE('',#2910,#2907,#1892,.T.);
#3769=EDGE_CURVE('',#2911,#2909,#1893,.T.);
#3770=EDGE_CURVE('',#2911,#2912,#1894,.T.);
#3771=EDGE_CURVE('',#2912,#2910,#1895,.T.);
#3772=EDGE_CURVE('',#2913,#2911,#1896,.T.);
#3773=EDGE_CURVE('',#2913,#2914,#1897,.T.);
#3774=EDGE_CURVE('',#2914,#2912,#1898,.T.);
#3775=EDGE_CURVE('',#2915,#2913,#1899,.T.);
#3776=EDGE_CURVE('',#2915,#2916,#1900,.T.);
#3777=EDGE_CURVE('',#2916,#2914,#1901,.T.);
#3778=EDGE_CURVE('',#2906,#2915,#1902,.T.);
#3779=EDGE_CURVE('',#2908,#2916,#1903,.T.);
#3780=EDGE_CURVE('',#2917,#2917,#1145,.T.);
#3781=EDGE_CURVE('',#2917,#2918,#1904,.T.);
#3782=EDGE_CURVE('',#2918,#2918,#1146,.T.);
#5255=ORIENTED_EDGE('',*,*,#3687,.F.);
#5256=ORIENTED_EDGE('',*,*,#3688,.T.);
#5257=ORIENTED_EDGE('',*,*,#3689,.T.);
#5258=ORIENTED_EDGE('',*,*,#3690,.T.);
#5259=ORIENTED_EDGE('',*,*,#3691,.F.);
#5260=ORIENTED_EDGE('',*,*,#3692,.T.);
#5261=ORIENTED_EDGE('',*,*,#3687,.T.);
#5262=ORIENTED_EDGE('',*,*,#3693,.T.);
#5263=ORIENTED_EDGE('',*,*,#3694,.F.);
#5264=ORIENTED_EDGE('',*,*,#3695,.T.);
#5265=ORIENTED_EDGE('',*,*,#3691,.T.);
#5266=ORIENTED_EDGE('',*,*,#3696,.T.);
#5267=ORIENTED_EDGE('',*,*,#3697,.F.);
#5268=ORIENTED_EDGE('',*,*,#3698,.T.);
#5269=ORIENTED_EDGE('',*,*,#3694,.T.);
#5270=ORIENTED_EDGE('',*,*,#3699,.T.);
#5271=ORIENTED_EDGE('',*,*,#3700,.F.);
#5272=ORIENTED_EDGE('',*,*,#3701,.T.);
#5273=ORIENTED_EDGE('',*,*,#3697,.T.);
#5274=ORIENTED_EDGE('',*,*,#3702,.T.);
#5275=ORIENTED_EDGE('',*,*,#3703,.F.);
#5276=ORIENTED_EDGE('',*,*,#3704,.T.);
#5277=ORIENTED_EDGE('',*,*,#3700,.T.);
#5278=ORIENTED_EDGE('',*,*,#3705,.T.);
#5279=ORIENTED_EDGE('',*,*,#3706,.F.);
#5280=ORIENTED_EDGE('',*,*,#3707,.T.);
#5281=ORIENTED_EDGE('',*,*,#3703,.T.);
#5282=ORIENTED_EDGE('',*,*,#3708,.T.);
#5283=ORIENTED_EDGE('',*,*,#3709,.F.);
#5284=ORIENTED_EDGE('',*,*,#3710,.T.);
#5285=ORIENTED_EDGE('',*,*,#3706,.T.);
#5286=ORIENTED_EDGE('',*,*,#3711,.T.);
#5287=ORIENTED_EDGE('',*,*,#3712,.F.);
#5288=ORIENTED_EDGE('',*,*,#3713,.T.);
#5289=ORIENTED_EDGE('',*,*,#3709,.T.);
#5290=ORIENTED_EDGE('',*,*,#3714,.T.);
#5291=ORIENTED_EDGE('',*,*,#3715,.F.);
#5292=ORIENTED_EDGE('',*,*,#3716,.T.);
#5293=ORIENTED_EDGE('',*,*,#3712,.T.);
#5294=ORIENTED_EDGE('',*,*,#3717,.T.);
#5295=ORIENTED_EDGE('',*,*,#3718,.F.);
#5296=ORIENTED_EDGE('',*,*,#3719,.T.);
#5297=ORIENTED_EDGE('',*,*,#3720,.T.);
#5298=ORIENTED_EDGE('',*,*,#3721,.F.);
#5299=ORIENTED_EDGE('',*,*,#3722,.F.);
#5300=ORIENTED_EDGE('',*,*,#3723,.T.);
#5301=ORIENTED_EDGE('',*,*,#3718,.T.);
#5302=ORIENTED_EDGE('',*,*,#3724,.F.);
#5303=ORIENTED_EDGE('',*,*,#3725,.F.);
#5304=ORIENTED_EDGE('',*,*,#3726,.T.);
#5305=ORIENTED_EDGE('',*,*,#3722,.T.);
#5306=ORIENTED_EDGE('',*,*,#3727,.F.);
#5307=ORIENTED_EDGE('',*,*,#3728,.F.);
#5308=ORIENTED_EDGE('',*,*,#3729,.T.);
#5309=ORIENTED_EDGE('',*,*,#3725,.T.);
#5310=ORIENTED_EDGE('',*,*,#3730,.F.);
#5311=ORIENTED_EDGE('',*,*,#3731,.F.);
#5312=ORIENTED_EDGE('',*,*,#3732,.T.);
#5313=ORIENTED_EDGE('',*,*,#3728,.T.);
#5314=ORIENTED_EDGE('',*,*,#3733,.F.);
#5315=ORIENTED_EDGE('',*,*,#3734,.F.);
#5316=ORIENTED_EDGE('',*,*,#3735,.T.);
#5317=ORIENTED_EDGE('',*,*,#3731,.T.);
#5318=ORIENTED_EDGE('',*,*,#3736,.F.);
#5319=ORIENTED_EDGE('',*,*,#3737,.F.);
#5320=ORIENTED_EDGE('',*,*,#3738,.T.);
#5321=ORIENTED_EDGE('',*,*,#3734,.T.);
#5322=ORIENTED_EDGE('',*,*,#3739,.F.);
#5323=ORIENTED_EDGE('',*,*,#3740,.F.);
#5324=ORIENTED_EDGE('',*,*,#3741,.T.);
#5325=ORIENTED_EDGE('',*,*,#3737,.T.);
#5326=ORIENTED_EDGE('',*,*,#3742,.F.);
#5327=ORIENTED_EDGE('',*,*,#3743,.F.);
#5328=ORIENTED_EDGE('',*,*,#3744,.T.);
#5329=ORIENTED_EDGE('',*,*,#3740,.T.);
#5330=ORIENTED_EDGE('',*,*,#3745,.F.);
#5331=ORIENTED_EDGE('',*,*,#3746,.F.);
#5332=ORIENTED_EDGE('',*,*,#3747,.T.);
#5333=ORIENTED_EDGE('',*,*,#3743,.T.);
#5334=ORIENTED_EDGE('',*,*,#3748,.F.);
#5335=ORIENTED_EDGE('',*,*,#3749,.F.);
#5336=ORIENTED_EDGE('',*,*,#3720,.F.);
#5337=ORIENTED_EDGE('',*,*,#3750,.F.);
#5338=ORIENTED_EDGE('',*,*,#3751,.F.);
#5339=ORIENTED_EDGE('',*,*,#3752,.F.);
#5340=ORIENTED_EDGE('',*,*,#3753,.T.);
#5341=ORIENTED_EDGE('',*,*,#3754,.F.);
#5342=ORIENTED_EDGE('',*,*,#3753,.F.);
#5343=ORIENTED_EDGE('',*,*,#3750,.T.);
#5344=ORIENTED_EDGE('',*,*,#3719,.F.);
#5345=ORIENTED_EDGE('',*,*,#3723,.F.);
#5346=ORIENTED_EDGE('',*,*,#3726,.F.);
#5347=ORIENTED_EDGE('',*,*,#3729,.F.);
#5348=ORIENTED_EDGE('',*,*,#3732,.F.);
#5349=ORIENTED_EDGE('',*,*,#3735,.F.);
#5350=ORIENTED_EDGE('',*,*,#3738,.F.);
#5351=ORIENTED_EDGE('',*,*,#3741,.F.);
#5352=ORIENTED_EDGE('',*,*,#3744,.F.);
#5353=ORIENTED_EDGE('',*,*,#3747,.F.);
#5354=ORIENTED_EDGE('',*,*,#3755,.F.);
#5355=ORIENTED_EDGE('',*,*,#3756,.F.);
#5356=ORIENTED_EDGE('',*,*,#3688,.F.);
#5357=ORIENTED_EDGE('',*,*,#3692,.F.);
#5358=ORIENTED_EDGE('',*,*,#3695,.F.);
#5359=ORIENTED_EDGE('',*,*,#3698,.F.);
#5360=ORIENTED_EDGE('',*,*,#3701,.F.);
#5361=ORIENTED_EDGE('',*,*,#3704,.F.);
#5362=ORIENTED_EDGE('',*,*,#3707,.F.);
#5363=ORIENTED_EDGE('',*,*,#3710,.F.);
#5364=ORIENTED_EDGE('',*,*,#3713,.F.);
#5365=ORIENTED_EDGE('',*,*,#3716,.F.);
#5366=ORIENTED_EDGE('',*,*,#3757,.F.);
#5367=ORIENTED_EDGE('',*,*,#3746,.T.);
#5368=ORIENTED_EDGE('',*,*,#3758,.F.);
#5369=ORIENTED_EDGE('',*,*,#3759,.F.);
#5370=ORIENTED_EDGE('',*,*,#3755,.T.);
#5371=ORIENTED_EDGE('',*,*,#3749,.T.);
#5372=ORIENTED_EDGE('',*,*,#3752,.T.);
#5373=ORIENTED_EDGE('',*,*,#3760,.F.);
#5374=ORIENTED_EDGE('',*,*,#3717,.F.);
#5375=ORIENTED_EDGE('',*,*,#3714,.F.);
#5376=ORIENTED_EDGE('',*,*,#3711,.F.);
#5377=ORIENTED_EDGE('',*,*,#3708,.F.);
#5378=ORIENTED_EDGE('',*,*,#3705,.F.);
#5379=ORIENTED_EDGE('',*,*,#3702,.F.);
#5380=ORIENTED_EDGE('',*,*,#3699,.F.);
#5381=ORIENTED_EDGE('',*,*,#3696,.F.);
#5382=ORIENTED_EDGE('',*,*,#3693,.F.);
#5383=ORIENTED_EDGE('',*,*,#3690,.F.);
#5384=ORIENTED_EDGE('',*,*,#3761,.F.);
#5385=ORIENTED_EDGE('',*,*,#3758,.T.);
#5386=ORIENTED_EDGE('',*,*,#3748,.T.);
#5387=ORIENTED_EDGE('',*,*,#3745,.T.);
#5388=ORIENTED_EDGE('',*,*,#3742,.T.);
#5389=ORIENTED_EDGE('',*,*,#3739,.T.);
#5390=ORIENTED_EDGE('',*,*,#3736,.T.);
#5391=ORIENTED_EDGE('',*,*,#3733,.T.);
#5392=ORIENTED_EDGE('',*,*,#3730,.T.);
#5393=ORIENTED_EDGE('',*,*,#3727,.T.);
#5394=ORIENTED_EDGE('',*,*,#3724,.T.);
#5395=ORIENTED_EDGE('',*,*,#3721,.T.);
#5396=ORIENTED_EDGE('',*,*,#3715,.T.);
#5397=ORIENTED_EDGE('',*,*,#3760,.T.);
#5398=ORIENTED_EDGE('',*,*,#3751,.T.);
#5399=ORIENTED_EDGE('',*,*,#3757,.T.);
#5400=ORIENTED_EDGE('',*,*,#3762,.F.);
#5401=ORIENTED_EDGE('',*,*,#3763,.T.);
#5402=ORIENTED_EDGE('',*,*,#3764,.T.);
#5403=ORIENTED_EDGE('',*,*,#3765,.F.);
#5404=ORIENTED_EDGE('',*,*,#3766,.F.);
#5405=ORIENTED_EDGE('',*,*,#3767,.T.);
#5406=ORIENTED_EDGE('',*,*,#3768,.T.);
#5407=ORIENTED_EDGE('',*,*,#3763,.F.);
#5408=ORIENTED_EDGE('',*,*,#3769,.F.);
#5409=ORIENTED_EDGE('',*,*,#3770,.T.);
#5410=ORIENTED_EDGE('',*,*,#3771,.T.);
#5411=ORIENTED_EDGE('',*,*,#3767,.F.);
#5412=ORIENTED_EDGE('',*,*,#3772,.F.);
#5413=ORIENTED_EDGE('',*,*,#3773,.T.);
#5414=ORIENTED_EDGE('',*,*,#3774,.T.);
#5415=ORIENTED_EDGE('',*,*,#3770,.F.);
#5416=ORIENTED_EDGE('',*,*,#3775,.F.);
#5417=ORIENTED_EDGE('',*,*,#3776,.T.);
#5418=ORIENTED_EDGE('',*,*,#3777,.T.);
#5419=ORIENTED_EDGE('',*,*,#3773,.F.);
#5420=ORIENTED_EDGE('',*,*,#3778,.F.);
#5421=ORIENTED_EDGE('',*,*,#3765,.T.);
#5422=ORIENTED_EDGE('',*,*,#3779,.T.);
#5423=ORIENTED_EDGE('',*,*,#3776,.F.);
#5424=ORIENTED_EDGE('',*,*,#3779,.F.);
#5425=ORIENTED_EDGE('',*,*,#3764,.F.);
#5426=ORIENTED_EDGE('',*,*,#3768,.F.);
#5427=ORIENTED_EDGE('',*,*,#3771,.F.);
#5428=ORIENTED_EDGE('',*,*,#3774,.F.);
#5429=ORIENTED_EDGE('',*,*,#3777,.F.);
#5430=ORIENTED_EDGE('',*,*,#3780,.T.);
#5431=ORIENTED_EDGE('',*,*,#3756,.T.);
#5432=ORIENTED_EDGE('',*,*,#3759,.T.);
#5433=ORIENTED_EDGE('',*,*,#3761,.T.);
#5434=ORIENTED_EDGE('',*,*,#3689,.F.);
#5435=ORIENTED_EDGE('',*,*,#3780,.F.);
#5436=ORIENTED_EDGE('',*,*,#3781,.T.);
#5437=ORIENTED_EDGE('',*,*,#3782,.T.);
#5438=ORIENTED_EDGE('',*,*,#3781,.F.);
#5439=ORIENTED_EDGE('',*,*,#3782,.F.);
#5440=ORIENTED_EDGE('',*,*,#3762,.T.);
#5441=ORIENTED_EDGE('',*,*,#3778,.T.);
#5442=ORIENTED_EDGE('',*,*,#3775,.T.);
#5443=ORIENTED_EDGE('',*,*,#3772,.T.);
#5444=ORIENTED_EDGE('',*,*,#3769,.T.);
#5445=ORIENTED_EDGE('',*,*,#3766,.T.);
#5446=ORIENTED_EDGE('',*,*,#3754,.T.);
#5965=CYLINDRICAL_SURFACE('',#6823,1.954);
#5966=CYLINDRICAL_SURFACE('',#6825,1.954);
#5967=CYLINDRICAL_SURFACE('',#6826,1.954);
#5968=CYLINDRICAL_SURFACE('',#6827,1.954);
#5969=CYLINDRICAL_SURFACE('',#6828,1.954);
#5970=CYLINDRICAL_SURFACE('',#6829,1.954);
#5971=CYLINDRICAL_SURFACE('',#6830,1.954);
#5972=CYLINDRICAL_SURFACE('',#6831,1.954);
#5973=CYLINDRICAL_SURFACE('',#6832,1.954);
#5974=CYLINDRICAL_SURFACE('',#6833,1.954);
#5975=CYLINDRICAL_SURFACE('',#6834,1.5555);
#5976=CYLINDRICAL_SURFACE('',#6836,1.5555);
#5977=CYLINDRICAL_SURFACE('',#6837,1.5555);
#5978=CYLINDRICAL_SURFACE('',#6838,1.5555);
#5979=CYLINDRICAL_SURFACE('',#6839,1.5555);
#5980=CYLINDRICAL_SURFACE('',#6840,1.5555);
#5981=CYLINDRICAL_SURFACE('',#6841,1.5555);
#5982=CYLINDRICAL_SURFACE('',#6842,1.5555);
#5983=CYLINDRICAL_SURFACE('',#6843,1.5555);
#5984=CYLINDRICAL_SURFACE('',#6844,1.5555);
#5985=CYLINDRICAL_SURFACE('',#6848,1.5555);
#5986=CYLINDRICAL_SURFACE('',#6850,1.954);
#5987=CYLINDRICAL_SURFACE('',#6860,3.5);
#6273=ADVANCED_FACE('',(#561),#5965,.T.);
#6274=ADVANCED_FACE('',(#562),#5966,.T.);
#6275=ADVANCED_FACE('',(#563),#5967,.T.);
#6276=ADVANCED_FACE('',(#564),#5968,.T.);
#6277=ADVANCED_FACE('',(#565),#5969,.T.);
#6278=ADVANCED_FACE('',(#566),#5970,.T.);
#6279=ADVANCED_FACE('',(#567),#5971,.T.);
#6280=ADVANCED_FACE('',(#568),#5972,.T.);
#6281=ADVANCED_FACE('',(#569),#5973,.T.);
#6282=ADVANCED_FACE('',(#570),#5974,.T.);
#6283=ADVANCED_FACE('',(#571),#5975,.T.);
#6284=ADVANCED_FACE('',(#572),#5976,.T.);
#6285=ADVANCED_FACE('',(#573),#5977,.T.);
#6286=ADVANCED_FACE('',(#574),#5978,.T.);
#6287=ADVANCED_FACE('',(#575),#5979,.T.);
#6288=ADVANCED_FACE('',(#576),#5980,.T.);
#6289=ADVANCED_FACE('',(#577),#5981,.T.);
#6290=ADVANCED_FACE('',(#578),#5982,.T.);
#6291=ADVANCED_FACE('',(#579),#5983,.T.);
#6292=ADVANCED_FACE('',(#580),#5984,.T.);
#6293=ADVANCED_FACE('',(#581),#79,.T.);
#6294=ADVANCED_FACE('',(#582),#137,.F.);
#6295=ADVANCED_FACE('',(#583),#5985,.T.);
#6296=ADVANCED_FACE('',(#584),#138,.F.);
#6297=ADVANCED_FACE('',(#585),#5986,.T.);
#6298=ADVANCED_FACE('',(#586),#283,.F.);
#6299=ADVANCED_FACE('',(#587),#284,.F.);
#6300=ADVANCED_FACE('',(#588),#285,.F.);
#6301=ADVANCED_FACE('',(#589),#286,.F.);
#6302=ADVANCED_FACE('',(#590),#287,.F.);
#6303=ADVANCED_FACE('',(#591),#288,.F.);
#6304=ADVANCED_FACE('',(#592),#289,.F.);
#6305=ADVANCED_FACE('',(#593,#189),#290,.T.);
#6306=ADVANCED_FACE('',(#594),#5987,.T.);
#6307=ADVANCED_FACE('',(#595,#190),#291,.F.);
#6308=ADVANCED_FACE('',(#596),#292,.T.);
#6387=CLOSED_SHELL('',(#6273,#6274,#6275,#6276,#6277,#6278,#6279,#6280,
#6281,#6282,#6283,#6284,#6285,#6286,#6287,#6288,#6289,#6290,#6291,#6292,
#6293,#6294,#6295,#6296,#6297,#6298,#6299,#6300,#6301,#6302,#6303,#6304,
#6305,#6306,#6307,#6308));
#6822=AXIS2_PLACEMENT_3D('',#16347,#7943,#7944);
#6823=AXIS2_PLACEMENT_3D('',#16348,#7945,#7946);
#6824=AXIS2_PLACEMENT_3D('',#16364,#7948,#7949);
#6825=AXIS2_PLACEMENT_3D('',#16372,#7950,#7951);
#6826=AXIS2_PLACEMENT_3D('',#16420,#7953,#7954);
#6827=AXIS2_PLACEMENT_3D('',#16468,#7956,#7957);
#6828=AXIS2_PLACEMENT_3D('',#16519,#7959,#7960);
#6829=AXIS2_PLACEMENT_3D('',#16570,#7962,#7963);
#6830=AXIS2_PLACEMENT_3D('',#16618,#7965,#7966);
#6831=AXIS2_PLACEMENT_3D('',#16666,#7968,#7969);
#6832=AXIS2_PLACEMENT_3D('',#16720,#7971,#7972);
#6833=AXIS2_PLACEMENT_3D('',#16768,#7974,#7975);
#6834=AXIS2_PLACEMENT_3D('',#16816,#7977,#7978);
#6835=AXIS2_PLACEMENT_3D('',#16832,#7980,#7981);
#6836=AXIS2_PLACEMENT_3D('',#16841,#7982,#7983);
#6837=AXIS2_PLACEMENT_3D('',#16866,#7985,#7986);
#6838=AXIS2_PLACEMENT_3D('',#16890,#7988,#7989);
#6839=AXIS2_PLACEMENT_3D('',#16915,#7991,#7992);
#6840=AXIS2_PLACEMENT_3D('',#16940,#7994,#7995);
#6841=AXIS2_PLACEMENT_3D('',#16964,#7997,#7998);
#6842=AXIS2_PLACEMENT_3D('',#16988,#8000,#8001);
#6843=AXIS2_PLACEMENT_3D('',#17014,#8003,#8004);
#6844=AXIS2_PLACEMENT_3D('',#17038,#8006,#8007);
#6845=AXIS2_PLACEMENT_3D('',#17062,#8009,#8010);
#6846=AXIS2_PLACEMENT_3D('',#17329,#8011,#8012);
#6847=AXIS2_PLACEMENT_3D('',#17360,#8014,#8015);
#6848=AXIS2_PLACEMENT_3D('',#17754,#8016,#8017);
#6849=AXIS2_PLACEMENT_3D('',#17765,#8018,#8019);
#6850=AXIS2_PLACEMENT_3D('',#18158,#8020,#8021);
#6851=AXIS2_PLACEMENT_3D('',#18159,#8022,#8023);
#6852=AXIS2_PLACEMENT_3D('',#18168,#8028,#8029);
#6853=AXIS2_PLACEMENT_3D('',#18174,#8033,#8034);
#6854=AXIS2_PLACEMENT_3D('',#18180,#8038,#8039);
#6855=AXIS2_PLACEMENT_3D('',#18186,#8043,#8044);
#6856=AXIS2_PLACEMENT_3D('',#18192,#8048,#8049);
#6857=AXIS2_PLACEMENT_3D('',#18195,#8052,#8053);
#6858=AXIS2_PLACEMENT_3D('',#18196,#8054,#8055);
#6859=AXIS2_PLACEMENT_3D('',#18198,#8056,#8057);
#6860=AXIS2_PLACEMENT_3D('',#18199,#8058,#8059);
#6861=AXIS2_PLACEMENT_3D('',#18202,#8061,#8062);
#6862=AXIS2_PLACEMENT_3D('',#18203,#8063,#8064);
#6863=AXIS2_PLACEMENT_3D('',#18204,#8065,#8066);
#7943=DIRECTION('axis',(0.,0.,1.));
#7944=DIRECTION('refdir',(1.,0.,0.));
#7945=DIRECTION('center_axis',(0.,0.,1.));
#7946=DIRECTION('ref_axis',(1.,0.,0.));
#7947=DIRECTION('',(0.,0.,-1.));
#7948=DIRECTION('center_axis',(0.,0.,-1.));
#7949=DIRECTION('ref_axis',(1.,0.,0.));
#7950=DIRECTION('center_axis',(0.,0.,1.));
#7951=DIRECTION('ref_axis',(1.,0.,0.));
#7952=DIRECTION('',(0.,0.,-1.));
#7953=DIRECTION('center_axis',(0.,0.,1.));
#7954=DIRECTION('ref_axis',(1.,0.,0.));
#7955=DIRECTION('',(0.,0.,-1.));
#7956=DIRECTION('center_axis',(0.,0.,1.));
#7957=DIRECTION('ref_axis',(1.,0.,0.));
#7958=DIRECTION('',(0.,0.,-1.));
#7959=DIRECTION('center_axis',(0.,0.,1.));
#7960=DIRECTION('ref_axis',(1.,0.,0.));
#7961=DIRECTION('',(0.,0.,-1.));
#7962=DIRECTION('center_axis',(0.,0.,1.));
#7963=DIRECTION('ref_axis',(1.,0.,0.));
#7964=DIRECTION('',(0.,0.,-1.));
#7965=DIRECTION('center_axis',(0.,0.,1.));
#7966=DIRECTION('ref_axis',(1.,0.,0.));
#7967=DIRECTION('',(0.,0.,-1.));
#7968=DIRECTION('center_axis',(0.,0.,1.));
#7969=DIRECTION('ref_axis',(1.,0.,0.));
#7970=DIRECTION('',(0.,0.,-1.));
#7971=DIRECTION('center_axis',(0.,0.,1.));
#7972=DIRECTION('ref_axis',(1.,0.,0.));
#7973=DIRECTION('',(0.,0.,-1.));
#7974=DIRECTION('center_axis',(0.,0.,1.));
#7975=DIRECTION('ref_axis',(1.,0.,0.));
#7976=DIRECTION('',(0.,0.,-1.));
#7977=DIRECTION('center_axis',(0.,0.,1.));
#7978=DIRECTION('ref_axis',(0.99867308056793,-0.051498331516286,0.));
#7979=DIRECTION('',(0.,0.,1.));
#7980=DIRECTION('center_axis',(0.,0.,-1.));
#7981=DIRECTION('ref_axis',(1.,5.83250561478606E-14,0.));
#7982=DIRECTION('center_axis',(0.,0.,1.));
#7983=DIRECTION('ref_axis',(1.,5.83250561478606E-14,0.));
#7984=DIRECTION('',(0.,0.,1.));
#7985=DIRECTION('center_axis',(0.,0.,1.));
#7986=DIRECTION('ref_axis',(1.,5.83250561478606E-14,0.));
#7987=DIRECTION('',(0.,0.,1.));
#7988=DIRECTION('center_axis',(0.,0.,1.));
#7989=DIRECTION('ref_axis',(1.,5.83250561478606E-14,0.));
#7990=DIRECTION('',(0.,0.,1.));
#7991=DIRECTION('center_axis',(0.,0.,1.));
#7992=DIRECTION('ref_axis',(1.,5.83250561478606E-14,0.));
#7993=DIRECTION('',(0.,0.,1.));
#7994=DIRECTION('center_axis',(0.,0.,1.));
#7995=DIRECTION('ref_axis',(1.,5.83250561478606E-14,0.));
#7996=DIRECTION('',(0.,0.,1.));
#7997=DIRECTION('center_axis',(0.,0.,1.));
#7998=DIRECTION('ref_axis',(1.,5.83250561478606E-14,0.));
#7999=DIRECTION('',(0.,0.,1.));
#8000=DIRECTION('center_axis',(0.,0.,1.));
#8001=DIRECTION('ref_axis',(1.,5.83250561478606E-14,0.));
#8002=DIRECTION('',(0.,0.,1.));
#8003=DIRECTION('center_axis',(0.,0.,1.));
#8004=DIRECTION('ref_axis',(1.,5.83250561478606E-14,0.));
#8005=DIRECTION('',(0.,0.,1.));
#8006=DIRECTION('center_axis',(0.,0.,1.));
#8007=DIRECTION('ref_axis',(1.,5.83250561478606E-14,0.));
#8008=DIRECTION('',(0.,0.,1.));
#8009=DIRECTION('center_axis',(0.,0.,-1.));
#8010=DIRECTION('ref_axis',(1.,0.,0.));
#8011=DIRECTION('center_axis',(0.,0.,-1.));
#8012=DIRECTION('ref_axis',(1.,0.,0.));
#8013=DIRECTION('',(0.707106781186547,8.65956056235493E-17,0.707106781186548));
#8014=DIRECTION('center_axis',(0.,0.,1.));
#8015=DIRECTION('ref_axis',(1.,0.,0.));
#8016=DIRECTION('center_axis',(0.,0.,1.));
#8017=DIRECTION('ref_axis',(1.,5.83250561478606E-14,0.));
#8018=DIRECTION('center_axis',(0.,0.,-1.));
#8019=DIRECTION('ref_axis',(1.,5.83250561478606E-14,0.));
#8020=DIRECTION('center_axis',(0.,0.,1.));
#8021=DIRECTION('ref_axis',(1.,0.,0.));
#8022=DIRECTION('center_axis',(-1.60246890531964E-16,-1.,0.));
#8023=DIRECTION('ref_axis',(1.,-1.60246890531964E-16,0.));
#8024=DIRECTION('',(1.,-1.60246890531964E-16,0.));
#8025=DIRECTION('',(0.,0.,1.));
#8026=DIRECTION('',(1.,-1.60246890531964E-16,0.));
#8027=DIRECTION('',(0.,0.,1.));
#8028=DIRECTION('center_axis',(-0.866025403784439,-0.5,0.));
#8029=DIRECTION('ref_axis',(0.5,-0.866025403784439,0.));
#8030=DIRECTION('',(0.5,-0.866025403784439,0.));
#8031=DIRECTION('',(0.,0.,1.));
#8032=DIRECTION('',(0.5,-0.866025403784439,0.));
#8033=DIRECTION('center_axis',(-0.866025403784439,0.5,0.));
#8034=DIRECTION('ref_axis',(-0.5,-0.866025403784439,0.));
#8035=DIRECTION('',(-0.5,-0.866025403784439,0.));
#8036=DIRECTION('',(0.,0.,1.));
#8037=DIRECTION('',(-0.5,-0.866025403784439,0.));
#8038=DIRECTION('center_axis',(1.60246890531964E-16,1.,0.));
#8039=DIRECTION('ref_axis',(-1.,1.60246890531964E-16,0.));
#8040=DIRECTION('',(-1.,1.60246890531964E-16,0.));
#8041=DIRECTION('',(0.,0.,1.));
#8042=DIRECTION('',(-1.,1.60246890531964E-16,0.));
#8043=DIRECTION('center_axis',(0.866025403784439,0.5,0.));
#8044=DIRECTION('ref_axis',(-0.5,0.866025403784439,0.));
#8045=DIRECTION('',(-0.5,0.866025403784439,0.));
#8046=DIRECTION('',(0.,0.,1.));
#8047=DIRECTION('',(-0.5,0.866025403784439,0.));
#8048=DIRECTION('center_axis',(0.866025403784439,-0.5,0.));
#8049=DIRECTION('ref_axis',(0.5,0.866025403784439,0.));
#8050=DIRECTION('',(0.5,0.866025403784439,0.));
#8051=DIRECTION('',(0.5,0.866025403784439,0.));
#8052=DIRECTION('center_axis',(0.,0.,1.));
#8053=DIRECTION('ref_axis',(1.,0.,0.));
#8054=DIRECTION('center_axis',(0.,0.,1.));
#8055=DIRECTION('ref_axis',(1.,0.,0.));
#8056=DIRECTION('center_axis',(0.,0.,1.));
#8057=DIRECTION('ref_axis',(1.,0.,0.));
#8058=DIRECTION('center_axis',(0.,0.,1.));
#8059=DIRECTION('ref_axis',(1.,0.,0.));
#8060=DIRECTION('',(0.,0.,-1.));
#8061=DIRECTION('center_axis',(0.,0.,1.));
#8062=DIRECTION('ref_axis',(1.,0.,0.));
#8063=DIRECTION('center_axis',(0.,0.,1.));
#8064=DIRECTION('ref_axis',(1.,0.,0.));
#8065=DIRECTION('center_axis',(0.,0.,1.));
#8066=DIRECTION('ref_axis',(1.,0.,0.));
#16347=CARTESIAN_POINT('',(0.,0.,0.));
#16348=CARTESIAN_POINT('Origin',(0.,0.,0.));
#16349=CARTESIAN_POINT('',(-1.95633598837559,0.00127248296362327,0.22586969212423));
#16350=CARTESIAN_POINT('',(-1.95588590413641,0.00206796222160181,0.124130307875766));
#16351=CARTESIAN_POINT('',(-1.954,-2.39295984553393E-16,0.));
#16352=CARTESIAN_POINT('',(0.861525859670522,1.75382131162755,0.));
#16353=CARTESIAN_POINT('Ctrl Pts',(-1.95633598837559,0.00127248296362327,
0.22586969212423));
#16354=CARTESIAN_POINT('Ctrl Pts',(-1.95680065536751,0.06824838727295,0.222037687723474));
#16355=CARTESIAN_POINT('Ctrl Pts',(-1.95366001618977,0.135177367276064,
0.218205683322718));
#16356=CARTESIAN_POINT('Ctrl Pts',(-1.9467704464542,0.201714622162032,0.214373678921962));
#16357=CARTESIAN_POINT('Ctrl Pts',(-1.88018097341933,0.844814396182631,
0.177336365489126));
#16358=CARTESIAN_POINT('Ctrl Pts',(-1.46337681650964,1.45132029737704,0.140299052056291));
#16359=CARTESIAN_POINT('Ctrl Pts',(-0.886898775458456,1.74452597744752,
0.103261738623455));
#16360=CARTESIAN_POINT('Ctrl Pts',(-0.351149650411554,2.01701629862282,
0.0688411590823035));
#16361=CARTESIAN_POINT('Ctrl Pts',(0.32250805655704,2.01891265608728,0.0344205795411517));
#16362=CARTESIAN_POINT('Ctrl Pts',(0.863568564283469,1.75641400930303,6.50521303491303E-18));
#16363=CARTESIAN_POINT('',(-0.861525859670545,1.75382131162753,0.));
#16364=CARTESIAN_POINT('Origin',(0.,0.,0.));
#16365=CARTESIAN_POINT('Ctrl Pts',(-0.861525859670546,1.75382131162753,
1.07552855510562E-15));
#16366=CARTESIAN_POINT('Ctrl Pts',(-1.44517400349648,1.46711709294739,0.0370752371124262));
#16367=CARTESIAN_POINT('Ctrl Pts',(-1.86938639577653,0.868642989156275,
0.0741504742248514));
#16368=CARTESIAN_POINT('Ctrl Pts',(-1.94388330047271,0.2267475072264,0.111225711337276));
#16369=CARTESIAN_POINT('Ctrl Pts',(-1.95252655828524,0.15227369973538,0.115527243516773));
#16370=CARTESIAN_POINT('Ctrl Pts',(-1.95646228341413,0.0772153955205521,
0.119828775696269));
#16371=CARTESIAN_POINT('Ctrl Pts',(-1.95588590413641,0.00206796222160181,
0.124130307875766));
#16372=CARTESIAN_POINT('Origin',(0.,0.,0.));
#16373=CARTESIAN_POINT('',(-1.95128265771456,0.000979968443958618,0.92586969212423));
#16374=CARTESIAN_POINT('',(-1.95120671878141,0.0009421225145049,0.824130307875766));
#16375=CARTESIAN_POINT('',(-1.954,-2.39295984553393E-16,0.));
#16376=CARTESIAN_POINT('Ctrl Pts',(-1.95128265771456,0.000979968443958618,
0.92586969212423));
#16377=CARTESIAN_POINT('Ctrl Pts',(-1.95247392016078,0.26388492489574,0.910928234987155));
#16378=CARTESIAN_POINT('Ctrl Pts',(-1.90305890226364,0.526360198569273,
0.895986777850081));
#16379=CARTESIAN_POINT('Ctrl Pts',(-1.80091082202569,0.76639335768976,0.881045320713007));
#16380=CARTESIAN_POINT('Ctrl Pts',(-1.54770322455863,1.36139445209842,0.844008007280172));
#16381=CARTESIAN_POINT('Ctrl Pts',(-0.970472477077253,1.8184979102298,0.806970693847336));
#16382=CARTESIAN_POINT('Ctrl Pts',(-0.333275819998743,1.92861264524847,
0.7699333804145));
#16383=CARTESIAN_POINT('Ctrl Pts',(0.303920837079767,2.03872738026714,0.732896066981664));
#16384=CARTESIAN_POINT('Ctrl Pts',(1.00108340375541,1.8018533921731,0.695858753548828));
#16385=CARTESIAN_POINT('Ctrl Pts',(1.43928269883041,1.32632160988724,0.658821440115992));
#16386=CARTESIAN_POINT('Ctrl Pts',(1.87748199390539,0.850789827601394,0.621784126683156));
#16387=CARTESIAN_POINT('Ctrl Pts',(2.05671801737973,0.13660025112374,0.584746813250321));
#16388=CARTESIAN_POINT('Ctrl Pts',(1.89500736899678,-0.489477875405323,
0.547709499817485));
#16389=CARTESIAN_POINT('Ctrl Pts',(1.73329672061383,-1.11555600193439,0.510672186384649));
#16390=CARTESIAN_POINT('Ctrl Pts',(1.23063940037359,-1.65352267851487,0.473634872951813));
#16391=CARTESIAN_POINT('Ctrl Pts',(0.616962143929708,-1.85738653188124,
0.436597559518977));
#16392=CARTESIAN_POINT('Ctrl Pts',(0.00328488748583246,-2.06125038524761,
0.399560246086142));
#16393=CARTESIAN_POINT('Ctrl Pts',(-0.721412305161677,-1.93101141539988,
0.362522932653306));
#16394=CARTESIAN_POINT('Ctrl Pts',(-1.2255735069054,-1.52604510705262,0.32548561922047));
#16395=CARTESIAN_POINT('Ctrl Pts',(-1.67757250343746,-1.1629779682701,0.29228031018839));
#16396=CARTESIAN_POINT('Ctrl Pts',(-1.95230952873461,-0.579091046852653,
0.25907500115631));
#16397=CARTESIAN_POINT('Ctrl Pts',(-1.95633598837559,0.00127248296362327,
0.22586969212423));
#16398=CARTESIAN_POINT('Ctrl Pts',(-1.95588590413641,0.00206796222160181,
0.124130307875766));
#16399=CARTESIAN_POINT('Ctrl Pts',(-1.95149442603296,-0.570486119123227,
0.156904012808695));
#16400=CARTESIAN_POINT('Ctrl Pts',(-1.68517377795595,-1.14821417361252,
0.189677717741624));
#16401=CARTESIAN_POINT('Ctrl Pts',(-1.24335992644724,-1.51202006337354,
0.222451422674553));
#16402=CARTESIAN_POINT('Ctrl Pts',(-0.74355823061328,-1.92357529197494,
0.259526659786979));
#16403=CARTESIAN_POINT('Ctrl Pts',(-0.0191734218330693,-2.06136888910912,
0.296601896899404));
#16404=CARTESIAN_POINT('Ctrl Pts',(0.59730918482247,-1.86366268614966,0.33367713401183));
#16405=CARTESIAN_POINT('Ctrl Pts',(1.21379179147801,-1.6659564831902,0.370752371124255));
#16406=CARTESIAN_POINT('Ctrl Pts',(1.72237219600888,-1.13275048013712,0.40782760823668));
#16407=CARTESIAN_POINT('Ctrl Pts',(1.89021021423941,-0.507705222320547,
0.444902845349105));
#16408=CARTESIAN_POINT('Ctrl Pts',(2.05804823246995,0.117340035496022,0.481978082461531));
#16409=CARTESIAN_POINT('Ctrl Pts',(1.88514386440015,0.834224548076076,0.519053319573957));
#16410=CARTESIAN_POINT('Ctrl Pts',(1.45061079828058,1.31401352267999,0.556128556686382));
#16411=CARTESIAN_POINT('Ctrl Pts',(1.01607773216101,1.7938024972839,0.593203793798808));
#16412=CARTESIAN_POINT('Ctrl Pts',(0.319915967991662,2.03649593391168,0.630279030911233));
#16413=CARTESIAN_POINT('Ctrl Pts',(-0.318741968595543,1.93105881108975,
0.667354268023658));
#16414=CARTESIAN_POINT('Ctrl Pts',(-0.95739990518275,1.82562168826782,0.704429505136084));
#16415=CARTESIAN_POINT('Ctrl Pts',(-1.53855401418781,1.37205400599619,0.74150474224851));
#16416=CARTESIAN_POINT('Ctrl Pts',(-1.79588703923712,0.778131328327298,
0.778579979360935));
#16417=CARTESIAN_POINT('Ctrl Pts',(-1.9012727786294,0.534901837996683,0.793763422199212));
#16418=CARTESIAN_POINT('Ctrl Pts',(-1.95234877280959,0.268132669686638,
0.808946865037489));
#16419=CARTESIAN_POINT('Ctrl Pts',(-1.95120671878141,0.000942122514504899,
0.824130307875766));
#16420=CARTESIAN_POINT('Origin',(0.,0.,0.));
#16421=CARTESIAN_POINT('',(-1.95279514498571,-0.00168107824419284,1.62586969212423));
#16422=CARTESIAN_POINT('',(-1.95278388634516,-0.00168888116712579,1.52413030787576));
#16423=CARTESIAN_POINT('',(-1.954,-2.39295984553393E-16,0.));
#16424=CARTESIAN_POINT('Ctrl Pts',(-1.95279514498571,-0.00168107824419284,
1.62586969212423));
#16425=CARTESIAN_POINT('Ctrl Pts',(-1.94903681723145,0.45580829851081,1.59981878225084));
#16426=CARTESIAN_POINT('Ctrl Pts',(-1.78858836662353,0.915672122197071,
1.57376787237745));
#16427=CARTESIAN_POINT('Ctrl Pts',(-1.49506049969948,1.26310357403151,1.54771696250405));
#16428=CARTESIAN_POINT('Ctrl Pts',(-1.07774365121422,1.75705666974124,1.51067964907122));
#16429=CARTESIAN_POINT('Ctrl Pts',(-0.391431901374392,2.02374896425016,
1.47364233563838));
#16430=CARTESIAN_POINT('Ctrl Pts',(0.249914641927464,1.94117972705521,1.43660502220554));
#16431=CARTESIAN_POINT('Ctrl Pts',(0.891261185229321,1.85861048986026,1.39956770877271));
#16432=CARTESIAN_POINT('Ctrl Pts',(1.48764252199321,1.42677972096142,1.36253039533987));
#16433=CARTESIAN_POINT('Ctrl Pts',(1.76623794405498,0.843232102738223,1.32549308190704));
#16434=CARTESIAN_POINT('Ctrl Pts',(2.04483336611675,0.25968448451502,1.2884557684742));
#16435=CARTESIAN_POINT('Ctrl Pts',(2.0056428734764,-0.475579983032552,1.25141845504136));
#16436=CARTESIAN_POINT('Ctrl Pts',(1.66659475578394,-1.02620605156362,1.21438114160853));
#16437=CARTESIAN_POINT('Ctrl Pts',(1.32754663809148,-1.57683212009468,1.17734382817569));
#16438=CARTESIAN_POINT('Ctrl Pts',(0.688640895346918,-1.94281978960923,
1.14030651474286));
#16439=CARTESIAN_POINT('Ctrl Pts',(0.0421509461412053,-1.956746580861,1.10326920131002));
#16440=CARTESIAN_POINT('Ctrl Pts',(-0.604339003064511,-1.97067337211277,
1.06623188787719));
#16441=CARTESIAN_POINT('Ctrl Pts',(-1.25841315873137,-1.63253928510176,
1.02919457444435));
#16442=CARTESIAN_POINT('Ctrl Pts',(-1.62085801283843,-1.09702287625329,
0.992157261011514));
#16443=CARTESIAN_POINT('Ctrl Pts',(-1.83708669330173,-0.777542532858632,
0.970061404715753));
#16444=CARTESIAN_POINT('Ctrl Pts',(-1.94952098456712,-0.38781143817112,
0.947965548419991));
#16445=CARTESIAN_POINT('Ctrl Pts',(-1.95128265771456,0.000979968443958618,
0.92586969212423));
#16446=CARTESIAN_POINT('Ctrl Pts',(-1.95120671878141,0.000942122514504899,
0.824130307875766));
#16447=CARTESIAN_POINT('Ctrl Pts',(-1.94956008223784,-0.384298600093132,
0.846022102149914));
#16448=CARTESIAN_POINT('Ctrl Pts',(-1.83936019485534,-0.770415304222176,
0.867913896424062));
#16449=CARTESIAN_POINT('Ctrl Pts',(-1.62687654459384,-1.08811501975669,
0.889805690698211));
#16450=CARTESIAN_POINT('Ctrl Pts',(-1.26702108380771,-1.62616101710563,
0.926880927810636));
#16451=CARTESIAN_POINT('Ctrl Pts',(-0.613798221141896,-1.96797533873735,
0.963956164923062));
#16452=CARTESIAN_POINT('Ctrl Pts',(0.0333981997247413,-1.95692658607738,
1.00103140203549));
#16453=CARTESIAN_POINT('Ctrl Pts',(0.680594620591375,-1.94587783341741,
1.03810663914791));
#16454=CARTESIAN_POINT('Ctrl Pts',(1.32176459965883,-1.58196600646575,1.07518187626034));
#16455=CARTESIAN_POINT('Ctrl Pts',(1.66305355512094,-1.03196363523784,1.11225711337276));
#16456=CARTESIAN_POINT('Ctrl Pts',(2.00434251058304,-0.481961264009935,
1.14933235048519));
#16457=CARTESIAN_POINT('Ctrl Pts',(2.04575044243979,0.254131651494222,1.18640758759761));
#16458=CARTESIAN_POINT('Ctrl Pts',(1.76829659796069,0.838942597907999,1.22348282471004));
#16459=CARTESIAN_POINT('Ctrl Pts',(1.49084275348159,1.42375354432178,1.26055806182247));
#16460=CARTESIAN_POINT('Ctrl Pts',(0.894527132666635,1.85728252164517,1.29763329893489));
#16461=CARTESIAN_POINT('Ctrl Pts',(0.252653428905354,1.94083943808002,1.33470853604732));
#16462=CARTESIAN_POINT('Ctrl Pts',(-0.389220274855925,2.02439635451486,
1.37178377315974));
#16463=CARTESIAN_POINT('Ctrl Pts',(-1.07665206156353,1.75798121006115,1.40885901027217));
#16464=CARTESIAN_POINT('Ctrl Pts',(-1.49458024744687,1.26369474377317,1.44593424738459));
#16465=CARTESIAN_POINT('Ctrl Pts',(-1.78840024024692,0.916191869184958,
1.47199960088165));
#16466=CARTESIAN_POINT('Ctrl Pts',(-1.94901418738241,0.456060303888852,
1.49806495437871));
#16467=CARTESIAN_POINT('Ctrl Pts',(-1.95278388634516,-0.00168888116712579,
1.52413030787576));
#16468=CARTESIAN_POINT('Origin',(0.,0.,0.));
#16469=CARTESIAN_POINT('',(-1.95720013100772,4.01036975386895E-5,2.32586969212423));
#16470=CARTESIAN_POINT('',(-1.95721475873132,-4.18937055542429E-5,2.22413030787576));
#16471=CARTESIAN_POINT('',(-1.954,-2.39295984553393E-16,0.));
#16472=CARTESIAN_POINT('Ctrl Pts',(-1.95720013100772,4.01036975387313E-5,
2.32586969212423));
#16473=CARTESIAN_POINT('Ctrl Pts',(-1.95720078041499,0.00218844021348119,
2.32574664294735));
#16474=CARTESIAN_POINT('Ctrl Pts',(-1.95719754885173,0.00433677471760079,
2.32562359377048));
#16475=CARTESIAN_POINT('Ctrl Pts',(-1.95719043044659,0.00648509634279326,
2.3255005445936));
#16476=CARTESIAN_POINT('Ctrl Pts',(-1.9550478187754,0.653121371426419,2.28846323116077));
#16477=CARTESIAN_POINT('Ctrl Pts',(-1.60076274017474,1.2985908336322,2.25142591772793));
#16478=CARTESIAN_POINT('Ctrl Pts',(-1.05640644317236,1.64761702679965,2.2143886042951));
#16479=CARTESIAN_POINT('Ctrl Pts',(-0.512050146169983,1.9966432199671,2.17735129086226));
#16480=CARTESIAN_POINT('Ctrl Pts',(0.22237736923411,2.04922614409623,2.14031397742942));
#16481=CARTESIAN_POINT('Ctrl Pts',(0.810904901655155,1.78131122209933,2.10327666399659));
#16482=CARTESIAN_POINT('Ctrl Pts',(1.3994324340762,1.51339630010242,2.06623935056375));
#16483=CARTESIAN_POINT('Ctrl Pts',(1.8420599835142,0.924983531979483,2.02920203713092));
#16484=CARTESIAN_POINT('Ctrl Pts',(1.9363031541186,0.285248202840816,1.99216472369808));
#16485=CARTESIAN_POINT('Ctrl Pts',(2.030546324723,-0.354487126297849,1.95512741026525));
#16486=CARTESIAN_POINT('Ctrl Pts',(1.7764051164938,-1.04554501645225,1.91809009683241));
#16487=CARTESIAN_POINT('Ctrl Pts',(1.29013896790468,-1.47179410874122,1.88105278339957));
#16488=CARTESIAN_POINT('Ctrl Pts',(0.80387281931556,-1.8980432010302,1.84401546996674));
#16489=CARTESIAN_POINT('Ctrl Pts',(0.0854817303665232,-2.05948349545377,
1.8069781565339));
#16490=CARTESIAN_POINT('Ctrl Pts',(-0.536399128085272,-1.88226256360254,
1.76994084310107));
#16491=CARTESIAN_POINT('Ctrl Pts',(-1.15827998653706,-1.70504163175131,
1.73290352966823));
#16492=CARTESIAN_POINT('Ctrl Pts',(-1.68365061449161,-1.18915947362529,
1.69586621623539));
#16493=CARTESIAN_POINT('Ctrl Pts',(-1.87217495490353,-0.570611446107024,
1.65882890280256));
#16494=CARTESIAN_POINT('Ctrl Pts',(-1.92809705865707,-0.387131122580406,
1.64784249924311));
#16495=CARTESIAN_POINT('Ctrl Pts',(-1.95438013781773,-0.194617253664394,
1.63685609568367));
#16496=CARTESIAN_POINT('Ctrl Pts',(-1.95279514498571,-0.00168107824419272,
1.62586969212423));
#16497=CARTESIAN_POINT('Ctrl Pts',(-1.95278388634516,-0.00168888116712579,
1.52413030787576));
#16498=CARTESIAN_POINT('Ctrl Pts',(-1.95437618958592,-0.19503999965723,
1.53514019149113));
#16499=CARTESIAN_POINT('Ctrl Pts',(-1.92798468468382,-0.387966059069047,
1.5461500751065));
#16500=CARTESIAN_POINT('Ctrl Pts',(-1.87182792927594,-0.571799497056349,
1.55715995872187));
#16501=CARTESIAN_POINT('Ctrl Pts',(-1.68272284016263,-1.19084948347563,
1.5942351958343));
#16502=CARTESIAN_POINT('Ctrl Pts',(-1.15608807687694,-1.70679166819193,
1.63131043294672));
#16503=CARTESIAN_POINT('Ctrl Pts',(-0.533290099975553,-1.88316099335306,
1.66838567005915));
#16504=CARTESIAN_POINT('Ctrl Pts',(0.0895078769258353,-2.05953031851418,
1.70546090717157));
#16505=CARTESIAN_POINT('Ctrl Pts',(0.808469067442917,-1.89632678412012,
1.742536144284));
#16506=CARTESIAN_POINT('Ctrl Pts',(1.2940806434107,-1.46834921584087,1.77961138139642));
#16507=CARTESIAN_POINT('Ctrl Pts',(1.77969221937849,-1.04037164756162,1.81668661850885));
#16508=CARTESIAN_POINT('Ctrl Pts',(2.03195418079698,-0.347620045397172,
1.85376185562127));
#16509=CARTESIAN_POINT('Ctrl Pts',(1.93525024356178,0.292404819142093,1.8908370927337));
#16510=CARTESIAN_POINT('Ctrl Pts',(1.83854630632657,0.932429683681362,1.92791232984612));
#16511=CARTESIAN_POINT('Ctrl Pts',(1.39287647043767,1.51972781059545,1.96498756695855));
#16512=CARTESIAN_POINT('Ctrl Pts',(0.802499325163421,1.78512991495868,2.00206280407098));
#16513=CARTESIAN_POINT('Ctrl Pts',(0.212122179889179,2.05053201932191,2.0391380411834));
#16514=CARTESIAN_POINT('Ctrl Pts',(-0.522962274770398,1.99403810113428,
2.07621327829583));
#16515=CARTESIAN_POINT('Ctrl Pts',(-1.06585153299182,1.64154030157863,2.11328851540825));
#16516=CARTESIAN_POINT('Ctrl Pts',(-1.60686689507973,1.29025922210662,2.15023577956409));
#16517=CARTESIAN_POINT('Ctrl Pts',(-1.95701157491646,0.645014173540876,
2.18718304371993));
#16518=CARTESIAN_POINT('Ctrl Pts',(-1.95721475873132,-4.18937055542428E-5,
2.22413030787576));
#16519=CARTESIAN_POINT('Origin',(0.,0.,0.));
#16520=CARTESIAN_POINT('',(-1.95267861104158,0.0016552724044671,3.02586969212423));
#16521=CARTESIAN_POINT('',(-1.95290774954615,0.00171310729769101,2.92413030787577));
#16522=CARTESIAN_POINT('',(-1.954,-2.39295984553393E-16,0.));
#16523=CARTESIAN_POINT('Ctrl Pts',(-1.95267861104158,0.0016552724044671,
3.02586969212423));
#16524=CARTESIAN_POINT('Ctrl Pts',(-1.95426730228936,0.198943040570848,
3.01463719021104));
#16525=CARTESIAN_POINT('Ctrl Pts',(-1.92676912869608,0.39579823972063,3.00340468829784));
#16526=CARTESIAN_POINT('Ctrl Pts',(-1.8683524720406,0.583005555161783,2.99217218638465));
#16527=CARTESIAN_POINT('Ctrl Pts',(-1.67573322844129,1.20029065090429,2.95513487295181));
#16528=CARTESIAN_POINT('Ctrl Pts',(-1.14695545989861,1.71267996796991,2.91809755951898));
#16529=CARTESIAN_POINT('Ctrl Pts',(-0.523913838219462,1.88577589531095,
2.88106024608614));
#16530=CARTESIAN_POINT('Ctrl Pts',(0.0991277834596942,2.05887182265199,
2.84402293265331));
#16531=CARTESIAN_POINT('Ctrl Pts',(0.816433258275323,1.89267436026844,2.80698561922047));
#16532=CARTESIAN_POINT('Ctrl Pts',(1.29986403215874,1.463212197494,2.76994830578763));
#16533=CARTESIAN_POINT('Ctrl Pts',(1.78329480604215,1.03375003471956,2.7329109923548));
#16534=CARTESIAN_POINT('Ctrl Pts',(2.03285087899336,0.341023171554252,2.69587367892196));
#16535=CARTESIAN_POINT('Ctrl Pts',(1.93437033276029,-0.298073569575231,
2.65883636548913));
#16536=CARTESIAN_POINT('Ctrl Pts',(1.83588978652722,-0.93717031070472,2.62179905205629));
#16537=CARTESIAN_POINT('Ctrl Pts',(1.38937262110987,-1.52263692979838,2.58476173862346));
#16538=CARTESIAN_POINT('Ctrl Pts',(0.799082573852251,-1.7866458736405,2.54772442519062));
#16539=CARTESIAN_POINT('Ctrl Pts',(0.208792526594628,-2.05065481748262,
2.51068711175778));
#16540=CARTESIAN_POINT('Ctrl Pts',(-0.525270402503268,-1.99320608607321,
2.47364979832495));
#16541=CARTESIAN_POINT('Ctrl Pts',(-1.06730179468137,-1.64058017638776,
2.43661248489211));
#16542=CARTESIAN_POINT('Ctrl Pts',(-1.60753239434872,-1.28912579681371,
2.39969822063615));
#16543=CARTESIAN_POINT('Ctrl Pts',(-1.95700531140595,-0.644452316926743,
2.36278395638019));
#16544=CARTESIAN_POINT('Ctrl Pts',(-1.95720013100772,4.01036975386895E-5,
2.32586969212423));
#16545=CARTESIAN_POINT('Ctrl Pts',(-1.95721475873132,-4.18937055544587E-5,
2.22413030787576));
#16546=CARTESIAN_POINT('Ctrl Pts',(-1.95721546249205,-0.00227615201876484,
2.22425828083235));
#16547=CARTESIAN_POINT('Ctrl Pts',(-1.9572119680126,-0.00451040806477065,
2.22438625378894));
#16548=CARTESIAN_POINT('Ctrl Pts',(-1.95720426868303,-0.00674464962048316,
2.22451422674553));
#16549=CARTESIAN_POINT('Ctrl Pts',(-1.95497368436953,-0.654030120340289,
2.26158946385795));
#16550=CARTESIAN_POINT('Ctrl Pts',(-1.59981845395926,-1.30009938085624,
2.29866470097038));
#16551=CARTESIAN_POINT('Ctrl Pts',(-1.0545126575596,-1.64884719787949,2.33573993808281));
#16552=CARTESIAN_POINT('Ctrl Pts',(-0.509206861159936,-1.99759501490274,
2.37281517519523));
#16553=CARTESIAN_POINT('Ctrl Pts',(0.226249501229124,-2.04902138843328,
2.40989041230765));
#16554=CARTESIAN_POINT('Ctrl Pts',(0.81478345819529,-1.77955667339696,2.44696564942008));
#16555=CARTESIAN_POINT('Ctrl Pts',(1.40331741516146,-1.51009195836063,2.4840408865325));
#16556=CARTESIAN_POINT('Ctrl Pts',(1.84492896670473,-0.919736154757425,
2.52111612364493));
#16557=CARTESIAN_POINT('Ctrl Pts',(1.93721953774244,-0.279060025103992,
2.55819136075736));
#16558=CARTESIAN_POINT('Ctrl Pts',(2.02951010878015,0.361616104549433,2.59526659786978));
#16559=CARTESIAN_POINT('Ctrl Pts',(1.7724796993123,1.05261256025308,2.63234183498221));
#16560=CARTESIAN_POINT('Ctrl Pts',(1.28393000274363,1.47723315072179,2.66941707209463));
#16561=CARTESIAN_POINT('Ctrl Pts',(0.795380306174951,1.9018537411905,2.70649230920706));
#16562=CARTESIAN_POINT('Ctrl Pts',(0.0753113225054439,2.06009846642426,
2.74356754631949));
#16563=CARTESIAN_POINT('Ctrl Pts',(-0.546256289304822,1.87944090130045,
2.78064278343191));
#16564=CARTESIAN_POINT('Ctrl Pts',(-1.16782390111508,1.69878333617665,2.81771802054433));
#16565=CARTESIAN_POINT('Ctrl Pts',(-1.6908901410661,1.17922348069528,2.85479325765676));
#16566=CARTESIAN_POINT('Ctrl Pts',(-1.875724275851,0.558885028961709,2.89186849476918));
#16567=CARTESIAN_POINT('Ctrl Pts',(-1.92933673865706,0.37895142411412,2.90262243247138));
#16568=CARTESIAN_POINT('Ctrl Pts',(-1.95449266845916,0.190538998342851,
2.91337637017357));
#16569=CARTESIAN_POINT('Ctrl Pts',(-1.95290774954615,0.00171310729769108,
2.92413030787576));
#16570=CARTESIAN_POINT('Origin',(0.,0.,0.));
#16571=CARTESIAN_POINT('',(-1.95135045472565,-0.00103665430809308,3.72586969212423));
#16572=CARTESIAN_POINT('',(-1.95115009645722,-0.000862413589311458,3.62413030787577));
#16573=CARTESIAN_POINT('',(-1.954,-2.39295984553393E-16,0.));
#16574=CARTESIAN_POINT('Ctrl Pts',(-1.95135045472565,-0.00103665430809308,
3.72586969212423));
#16575=CARTESIAN_POINT('Ctrl Pts',(-1.94945762145185,0.39205003232945,3.70352773747472));
#16576=CARTESIAN_POINT('Ctrl Pts',(-1.83432541049109,0.786156754205215,
3.6811857828252));
#16577=CARTESIAN_POINT('Ctrl Pts',(-1.61355237927334,1.1077387582254,3.65884382817569));
#16578=CARTESIAN_POINT('Ctrl Pts',(-1.2475664983152,1.64084043460512,3.62180651474286));
#16579=CARTESIAN_POINT('Ctrl Pts',(-0.591266345378013,1.97463505701166,
3.58476920131002));
#16580=CARTESIAN_POINT('Ctrl Pts',(0.0551170192794968,1.95642494139715,
3.54773188787719));
#16581=CARTESIAN_POINT('Ctrl Pts',(0.701500383937021,1.93821482578265,3.51069457444435));
#16582=CARTESIAN_POINT('Ctrl Pts',(1.33796696031487,1.56799997214707,3.47365726101151));
#16583=CARTESIAN_POINT('Ctrl Pts',(1.67335875584854,1.01513886309221,3.43661994757868));
#16584=CARTESIAN_POINT('Ctrl Pts',(2.00875055138221,0.46227775403734,3.39958263414584));
#16585=CARTESIAN_POINT('Ctrl Pts',(2.04306756607169,-0.273229610436822,
3.36254532071301));
#16586=CARTESIAN_POINT('Ctrl Pts',(1.76061113877997,-0.854918040011614,
3.32550800728017));
#16587=CARTESIAN_POINT('Ctrl Pts',(1.47815471148825,-1.4366064695864,3.28847069384734));
#16588=CARTESIAN_POINT('Ctrl Pts',(0.878924842215338,-1.86447596426182,
3.2514333804145));
#16589=CARTESIAN_POINT('Ctrl Pts',(0.237045219929842,-1.94279335001325,
3.21439606698166));
#16590=CARTESIAN_POINT('Ctrl Pts',(-0.404834402355659,-2.02111073576468,
3.17735875354883));
#16591=CARTESIAN_POINT('Ctrl Pts',(-1.08936377765374,-1.74987601259212,
3.14032144011599));
#16592=CARTESIAN_POINT('Ctrl Pts',(-1.50339810597481,-1.25316821379613,
3.10328412668316));
#16593=CARTESIAN_POINT('Ctrl Pts',(-1.79186605396357,-0.907099615934405,
3.07747931516352));
#16594=CARTESIAN_POINT('Ctrl Pts',(-1.94902885620257,-0.451580677342798,
3.05167450364387));
#16595=CARTESIAN_POINT('Ctrl Pts',(-1.95267861104158,0.0016552724044671,
3.02586969212423));
#16596=CARTESIAN_POINT('Ctrl Pts',(-1.95290774954615,0.00171310729769101,
2.92413030787577));
#16597=CARTESIAN_POINT('Ctrl Pts',(-1.94902850769025,-0.460456467442357,
2.950451607286));
#16598=CARTESIAN_POINT('Ctrl Pts',(-1.78495210853218,-0.925103000270984,
2.97677290669623));
#16599=CARTESIAN_POINT('Ctrl Pts',(-1.48583543343396,-1.27396510910143,
3.00309420610646));
#16600=CARTESIAN_POINT('Ctrl Pts',(-1.06451042661324,-1.76535974744522,
3.04016944321889));
#16601=CARTESIAN_POINT('Ctrl Pts',(-0.375258383353002,-2.02703197614702,
3.07724468033131));
#16602=CARTESIAN_POINT('Ctrl Pts',(0.266023999143107,-1.93905267245523,
3.11431991744374));
#16603=CARTESIAN_POINT('Ctrl Pts',(0.907306381639212,-1.85107336876345,
3.15139515455616));
#16604=CARTESIAN_POINT('Ctrl Pts',(1.50061910337119,-1.4134425326781,3.18847039166859));
#16605=CARTESIAN_POINT('Ctrl Pts',(1.77403619606301,-0.826734304146555,
3.22554562878102));
#16606=CARTESIAN_POINT('Ctrl Pts',(2.04745328875484,-0.240026075615009,
3.26262086589344));
#16607=CARTESIAN_POINT('Ctrl Pts',(2.0009747524065,0.495759545362725,3.29969610300586));
#16608=CARTESIAN_POINT('Ctrl Pts',(1.65590254220004,1.04339867994717,3.33677134011829));
#16609=CARTESIAN_POINT('Ctrl Pts',(1.31083033199357,1.59103781453161,3.37384657723071));
#16610=CARTESIAN_POINT('Ctrl Pts',(0.667164447928974,1.95053046272276,3.41092181434314));
#16611=CARTESIAN_POINT('Ctrl Pts',(0.0199086246964731,1.9571146316129,3.44799705145557));
#16612=CARTESIAN_POINT('Ctrl Pts',(-0.627347198536033,1.96369880050304,
3.485072288568));
#16613=CARTESIAN_POINT('Ctrl Pts',(-1.27819296093644,1.61737449009216,3.52214752568042));
#16614=CARTESIAN_POINT('Ctrl Pts',(-1.63433425949862,1.07686840552899,3.55922276279284));
#16615=CARTESIAN_POINT('Ctrl Pts',(-1.8421662177247,0.761447423909083,3.58085861115382));
#16616=CARTESIAN_POINT('Ctrl Pts',(-1.94963677903995,0.379897976317775,
3.60249445951479));
#16617=CARTESIAN_POINT('Ctrl Pts',(-1.95115009645722,-0.000862413589311458,
3.62413030787577));
#16618=CARTESIAN_POINT('Origin',(0.,0.,0.));
#16619=CARTESIAN_POINT('',(-1.95645463735042,-0.00107680116258307,4.42586969212423));
#16620=CARTESIAN_POINT('',(-1.9560689354221,-0.00131000797615835,4.32413030787576));
#16621=CARTESIAN_POINT('',(-1.954,-2.39295984553393E-16,0.));
#16622=CARTESIAN_POINT('Ctrl Pts',(-1.95645463735042,-0.00107680116258307,
4.42586969212423));
#16623=CARTESIAN_POINT('Ctrl Pts',(-1.95257837355362,0.583548870363389,
4.3924182847384));
#16624=CARTESIAN_POINT('Ctrl Pts',(-1.67319437992126,1.17138871222795,4.35896687735257));
#16625=CARTESIAN_POINT('Ctrl Pts',(-1.21542355114692,1.53407367113183,4.32551546996674));
#16626=CARTESIAN_POINT('Ctrl Pts',(-0.70858085032514,1.93563753794803,4.2884781565339));
#16627=CARTESIAN_POINT('Ctrl Pts',(0.0169438143861521,2.0611871352921,4.25144084310107));
#16628=CARTESIAN_POINT('Ctrl Pts',(0.629251938590984,1.85328854601076,4.21440352966823));
#16629=CARTESIAN_POINT('Ctrl Pts',(1.24156006279581,1.64538995672942,4.1773662162354));
#16630=CARTESIAN_POINT('Ctrl Pts',(1.74065164649418,1.10404318082267,4.14032890280256));
#16631=CARTESIAN_POINT('Ctrl Pts',(1.89821225955213,0.476892707953959,4.10329158936972));
#16632=CARTESIAN_POINT('Ctrl Pts',(2.05577287261007,-0.15025776491475,4.06625427593688));
#16633=CARTESIAN_POINT('Ctrl Pts',(1.87180251502759,-0.86321193474541,4.02921696250405));
#16634=CARTESIAN_POINT('Ctrl Pts',(1.4304602644841,-1.33582179532369,3.99217964907122));
#16635=CARTESIAN_POINT('Ctrl Pts',(0.989118013940611,-1.80843165590198,
3.95514233563838));
#16636=CARTESIAN_POINT('Ctrl Pts',(0.290403870436121,-2.04069720722789,
3.91810502220554));
#16637=CARTESIAN_POINT('Ctrl Pts',(-0.346048402169674,-1.92636625294191,
3.88106770877271));
#16638=CARTESIAN_POINT('Ctrl Pts',(-0.982500674775478,-1.81203529865592,
3.84403039533987));
#16639=CARTESIAN_POINT('Ctrl Pts',(-1.55669107648259,-1.35110783875803,
3.80699308190704));
#16640=CARTESIAN_POINT('Ctrl Pts',(-1.80595047284659,-0.754439743632632,
3.7699557684742));
#16641=CARTESIAN_POINT('Ctrl Pts',(-1.9048495538052,-0.517698713581134,
3.75526040969088));
#16642=CARTESIAN_POINT('Ctrl Pts',(-1.95259546056833,-0.259588333590661,
3.74056505090755));
#16643=CARTESIAN_POINT('Ctrl Pts',(-1.95135045472565,-0.00103665430809308,
3.72586969212423));
#16644=CARTESIAN_POINT('Ctrl Pts',(-1.95115009645722,-0.000862413589311458,
3.62413030787577));
#16645=CARTESIAN_POINT('Ctrl Pts',(-1.95223000307885,-0.272573861314833,
3.63956969662722));
#16646=CARTESIAN_POINT('Ctrl Pts',(-1.89935350538763,-0.543883498707529,
3.65500908537867));
#16647=CARTESIAN_POINT('Ctrl Pts',(-1.79048714938831,-0.790474416076489,
3.67044847413012));
#16648=CARTESIAN_POINT('Ctrl Pts',(-1.52906190599187,-1.38262329440335,
3.70752371124255));
#16649=CARTESIAN_POINT('Ctrl Pts',(-0.944774584475045,-1.83223319234163,
3.74459894835497));
#16650=CARTESIAN_POINT('Ctrl Pts',(-0.305414648672952,-1.93323974896447,
3.7816741854674));
#16651=CARTESIAN_POINT('Ctrl Pts',(0.333945287129141,-2.0342463055873,3.81874942257982));
#16652=CARTESIAN_POINT('Ctrl Pts',(1.0283778372165,-1.7866495208947,3.85582465969225));
#16653=CARTESIAN_POINT('Ctrl Pts',(1.45961198421181,-1.30392748653653,3.89289989680467));
#16654=CARTESIAN_POINT('Ctrl Pts',(1.89084613120712,-0.821205452178361,
3.9299751339171));
#16655=CARTESIAN_POINT('Ctrl Pts',(2.05888187511037,-0.103358168154617,
3.96705037102952));
#16656=CARTESIAN_POINT('Ctrl Pts',(1.88670539052006,0.520611951436678,4.00412560814195));
#16657=CARTESIAN_POINT('Ctrl Pts',(1.71452890592974,1.14458207102797,4.04120084525437));
#16658=CARTESIAN_POINT('Ctrl Pts',(1.20214019284586,1.67467502618682,4.0782760823668));
#16659=CARTESIAN_POINT('Ctrl Pts',(0.58437628040953,1.8679396129137,4.11535131947923));
#16660=CARTESIAN_POINT('Ctrl Pts',(-0.0333876320267997,2.06120419964058,
4.15242655659165));
#16661=CARTESIAN_POINT('Ctrl Pts',(-0.756526743815583,1.9176404179355,4.18950179370408));
#16662=CARTESIAN_POINT('Ctrl Pts',(-1.25361330032381,1.50304614961146,4.2265770308165));
#16663=CARTESIAN_POINT('Ctrl Pts',(-1.68959543059256,1.13941593283223,4.25909478983626));
#16664=CARTESIAN_POINT('Ctrl Pts',(-1.95168429546986,0.567292711935832,
4.29161254885601));
#16665=CARTESIAN_POINT('Ctrl Pts',(-1.9560689354221,-0.00131000797615835,
4.32413030787576));
#16666=CARTESIAN_POINT('Origin',(0.,0.,0.));
#16667=CARTESIAN_POINT('',(-1.95458552907139,0.00173412683576277,5.12586969212423));
#16668=CARTESIAN_POINT('',(-1.9552206747184,0.00161939276430114,5.02413030787577));
#16669=CARTESIAN_POINT('',(-1.954,-2.39295984553393E-16,0.));
#16670=CARTESIAN_POINT('Ctrl Pts',(-1.95458552907139,0.00173412683576277,
5.12586969212423));
#16671=CARTESIAN_POINT('Ctrl Pts',(-1.95579889273049,0.133549336413818,
5.11834614543492));
#16672=CARTESIAN_POINT('Ctrl Pts',(-1.94360248016884,0.265141296927549,
5.11082259874561));
#16673=CARTESIAN_POINT('Ctrl Pts',(-1.91717253101555,0.393809524200435,
5.10329905205629));
#16674=CARTESIAN_POINT('Ctrl Pts',(-1.78706177989932,1.02722427646379,5.06626173862345));
#16675=CARTESIAN_POINT('Ctrl Pts',(-1.31200866513269,1.58978387278703,5.02922442519062));
#16676=CARTESIAN_POINT('Ctrl Pts',(-0.709330998225857,1.82413979092323,
4.99218711175778));
#16677=CARTESIAN_POINT('Ctrl Pts',(-0.106653331319023,2.05849570905944,
4.95514979832495));
#16678=CARTESIAN_POINT('Ctrl Pts',(0.623648887728016,1.96464794900861,4.91811248489211));
#16679=CARTESIAN_POINT('Ctrl Pts',(1.14749162443816,1.58552811433593,4.88107517145928));
#16680=CARTESIAN_POINT('Ctrl Pts',(1.67133436114829,1.20640827966324,4.84403785802644));
#16681=CARTESIAN_POINT('Ctrl Pts',(1.98871761552153,0.542016370368706,4.8070005445936));
#16682=CARTESIAN_POINT('Ctrl Pts',(1.95445124244436,-0.103714902901561,
4.76996323116077));
#16683=CARTESIAN_POINT('Ctrl Pts',(1.9201848693672,-0.749446176171828,4.73292591772793));
#16684=CARTESIAN_POINT('Ctrl Pts',(1.53426886883963,-1.37651681341782,4.6958886042951));
#16685=CARTESIAN_POINT('Ctrl Pts',(0.973244372713117,-1.69806708597997,
4.65885129086226));
#16686=CARTESIAN_POINT('Ctrl Pts',(0.412219876586598,-2.01961735854213,
4.62181397742943));
#16687=CARTESIAN_POINT('Ctrl Pts',(-0.323913115138867,-2.03564726642044,
4.58477666399659));
#16688=CARTESIAN_POINT('Ctrl Pts',(-0.898403214163087,-1.7388237693533,
4.54773935056375));
#16689=CARTESIAN_POINT('Ctrl Pts',(-1.4728933131873,-1.44200027228616,4.51070203713092));
#16690=CARTESIAN_POINT('Ctrl Pts',(-1.88574051951028,-0.832323370273586,
4.47366472369808));
#16691=CARTESIAN_POINT('Ctrl Pts',(-1.94808375420563,-0.188695851123138,
4.43662741026525));
#16692=CARTESIAN_POINT('Ctrl Pts',(-1.95411974768256,-0.126380645212594,
4.43304150421824));
#16693=CARTESIAN_POINT('Ctrl Pts',(-1.95687016300016,-0.0637471906795113,
4.42945559817124));
#16694=CARTESIAN_POINT('Ctrl Pts',(-1.95645463735042,-0.00107680116258307,
4.42586969212423));
#16695=CARTESIAN_POINT('Ctrl Pts',(-1.9560689354221,-0.00131000797615835,
4.32413030787576));
#16696=CARTESIAN_POINT('Ctrl Pts',(-1.95668345810536,-0.0810016754695383,
4.32868778596844));
#16697=CARTESIAN_POINT('Ctrl Pts',(-1.95223589499426,-0.160624189738801,
4.33324526406111));
#16698=CARTESIAN_POINT('Ctrl Pts',(-1.94249551147141,-0.239593869899598,
4.33780274215378));
#16699=CARTESIAN_POINT('Ctrl Pts',(-1.86325716488311,-0.882014866143589,
4.3748779792662));
#16700=CARTESIAN_POINT('Ctrl Pts',(-1.43374647047883,-1.48123210368856,
4.41195321637863));
#16701=CARTESIAN_POINT('Ctrl Pts',(-0.850815960071711,-1.76261346774659,
4.44902845349105));
#16702=CARTESIAN_POINT('Ctrl Pts',(-0.267885449664584,-2.04399483180463,
4.48610369060348));
#16703=CARTESIAN_POINT('Ctrl Pts',(0.468464876745396,-2.00754032237573,
4.52317892771591));
#16704=CARTESIAN_POINT('Ctrl Pts',(1.02075232548754,-1.66995770146661,4.56025416482833));
#16705=CARTESIAN_POINT('Ctrl Pts',(1.57303977422969,-1.3323750805575,4.59732940194076));
#16706=CARTESIAN_POINT('Ctrl Pts',(1.941264345304,-0.693664348168167,4.63440463905318));
#16707=CARTESIAN_POINT('Ctrl Pts',(1.95666204750888,-0.0465582032952289,
4.67147987616561));
#16708=CARTESIAN_POINT('Ctrl Pts',(1.97205974971376,0.6005479415777,4.70855511327803));
#16709=CARTESIAN_POINT('Ctrl Pts',(1.63463058304921,1.25604949893424,4.74563035039046));
#16710=CARTESIAN_POINT('Ctrl Pts',(1.09902444690466,1.61951823074648,4.78270558750289));
#16711=CARTESIAN_POINT('Ctrl Pts',(0.56341831076011,1.98298696255872,4.81978082461531));
#16712=CARTESIAN_POINT('Ctrl Pts',(-0.170364794864445,2.05442286882665,
4.85685606172773));
#16713=CARTESIAN_POINT('Ctrl Pts',(-0.766018779707725,1.80108557937185,
4.89393129884016));
#16714=CARTESIAN_POINT('Ctrl Pts',(-1.361672764551,1.54774828991705,4.93100653595259));
#16715=CARTESIAN_POINT('Ctrl Pts',(-1.81919762861299,0.96963780473953,4.96808177306502));
#16716=CARTESIAN_POINT('Ctrl Pts',(-1.92890143946537,0.331712632206103,
5.00515701017744));
#16717=CARTESIAN_POINT('Ctrl Pts',(-1.9476151256888,0.222892971156397,5.01148144274355));
#16718=CARTESIAN_POINT('Ctrl Pts',(-1.95620763248682,0.112332773766476,
5.01780587530966));
#16719=CARTESIAN_POINT('Ctrl Pts',(-1.9552206747184,0.00161939276430114,
5.02413030787577));
#16720=CARTESIAN_POINT('Origin',(0.,0.,0.));
#16721=CARTESIAN_POINT('',(-1.95079790389112,-3.269510144494E-5,5.82586969212423));
#16722=CARTESIAN_POINT('',(-1.95085192255358,0.000383174536113729,5.72413030787576));
#16723=CARTESIAN_POINT('',(-1.954,-2.39295984553393E-16,0.));
#16724=CARTESIAN_POINT('Ctrl Pts',(-1.95079807093469,-3.26933958413878E-5,
5.82586969212423));
#16725=CARTESIAN_POINT('Ctrl Pts',(-1.95074883721548,0.328029941286317,
5.8072366926986));
#16726=CARTESIAN_POINT('Ctrl Pts',(-1.87242650231768,0.656114687980161,
5.78860369327296));
#16727=CARTESIAN_POINT('Ctrl Pts',(-1.71596284018057,0.941333347646706,
5.76997069384733));
#16728=CARTESIAN_POINT('Ctrl Pts',(-1.40495581640267,1.50827013831881,5.7329333804145));
#16729=CARTESIAN_POINT('Ctrl Pts',(-0.785207871169114,1.90584052998572,
5.69589606698167));
#16730=CARTESIAN_POINT('Ctrl Pts',(-0.140229809906548,1.95217121547304,
5.65885875354883));
#16731=CARTESIAN_POINT('Ctrl Pts',(0.504748251356019,1.99850190096035,5.62182144011599));
#16732=CARTESIAN_POINT('Ctrl Pts',(1.1749564286476,1.69359288026805,5.58478412668316));
#16733=CARTESIAN_POINT('Ctrl Pts',(1.56380177877164,1.17692822962597,5.54774681325032));
#16734=CARTESIAN_POINT('Ctrl Pts',(1.95264712889569,0.660263578983889,5.51070949981748));
#16735=CARTESIAN_POINT('Ctrl Pts',(2.06012965185219,-0.068156701607988,
5.47367218638465));
#16736=CARTESIAN_POINT('Ctrl Pts',(1.83708014107304,-0.675109688693547,
5.43663487295181));
#16737=CARTESIAN_POINT('Ctrl Pts',(1.61403063029389,-1.2820626757791,5.39959755951898));
#16738=CARTESIAN_POINT('Ctrl Pts',(1.06044908577908,-1.76754836935834,5.36256024608614));
#16739=CARTESIAN_POINT('Ctrl Pts',(0.429577047133733,-1.90947637973667,
5.32552293265331));
#16740=CARTESIAN_POINT('Ctrl Pts',(-0.201294991511623,-2.051404390115,5.28848561922047));
#16741=CARTESIAN_POINT('Ctrl Pts',(-0.909457524287529,-1.84977471729243,
5.25144830578764));
#16742=CARTESIAN_POINT('Ctrl Pts',(-1.37095459694257,-1.39682492677941,
5.2144109923548));
#16743=CARTESIAN_POINT('Ctrl Pts',(-1.73870581031982,-1.03588474984214,
5.18489722561128));
#16744=CARTESIAN_POINT('Ctrl Pts',(-1.94982568195559,-0.515357546731067,
5.15538345886775));
#16745=CARTESIAN_POINT('Ctrl Pts',(-1.95458552907139,0.00173412683576277,
5.12586969212423));
#16746=CARTESIAN_POINT('Ctrl Pts',(-1.9552206747184,0.00161939276430114,
5.02413030787577));
#16747=CARTESIAN_POINT('Ctrl Pts',(-1.95042186547898,-0.536693808344559,
5.05488111242208));
#16748=CARTESIAN_POINT('Ctrl Pts',(-1.71915285367837,-1.07862845650355,
5.0856319169684));
#16749=CARTESIAN_POINT('Ctrl Pts',(-1.32368315644793,-1.44172013107889,
5.11638272151471));
#16750=CARTESIAN_POINT('Ctrl Pts',(-0.846878304935377,-1.87948786194111,
5.15345795862714));
#16751=CARTESIAN_POINT('Ctrl Pts',(-0.131385844267519,-2.0572834637762,
5.19053319573957));
#16752=CARTESIAN_POINT('Ctrl Pts',(0.494871066573067,-1.89361998960963,
5.22760843285199));
#16753=CARTESIAN_POINT('Ctrl Pts',(1.12112797741365,-1.72995651544305,5.26468366996442));
#16754=CARTESIAN_POINT('Ctrl Pts',(1.65814933842698,-1.22483396527481,5.30175890707684));
#16755=CARTESIAN_POINT('Ctrl Pts',(1.85980853758091,-0.609759157741489,
5.33883414418927));
#16756=CARTESIAN_POINT('Ctrl Pts',(2.06146773673485,0.00531564979182955,
5.37590938130169));
#16757=CARTESIAN_POINT('Ctrl Pts',(1.9277647740294,0.730342714690214,5.41298461841412));
#16758=CARTESIAN_POINT('Ctrl Pts',(1.51997812810125,1.23302900604299,5.45005985552654));
#16759=CARTESIAN_POINT('Ctrl Pts',(1.11219148217311,1.73571529739576,5.48713509263897));
#16760=CARTESIAN_POINT('Ctrl Pts',(0.430321153022272,2.01606081520293,5.52421032975139));
#16761=CARTESIAN_POINT('Ctrl Pts',(-0.213119314048168,1.94557811718459,
5.56128556686382));
#16762=CARTESIAN_POINT('Ctrl Pts',(-0.856559781118622,1.87509541916625,
5.59836080397625));
#16763=CARTESIAN_POINT('Ctrl Pts',(-1.46157038610868,1.45378450532239,5.63543604108868));
#16764=CARTESIAN_POINT('Ctrl Pts',(-1.75086384963453,0.874739824296975,
5.6725112782011));
#16765=CARTESIAN_POINT('Ctrl Pts',(-1.88512280557994,0.606009472173862,
5.68971762142599));
#16766=CARTESIAN_POINT('Ctrl Pts',(-1.95138199037298,0.30330611490569,5.70692396465088));
#16767=CARTESIAN_POINT('Ctrl Pts',(-1.95085192255358,0.000383174536113729,
5.72413030787576));
#16768=CARTESIAN_POINT('Origin',(0.,0.,0.));
#16769=CARTESIAN_POINT('',(-1.95467666345581,-0.00169153748172557,6.52586969212423));
#16770=CARTESIAN_POINT('',(-1.95381346134878,-0.0017935399644829,6.42413030787577));
#16771=CARTESIAN_POINT('',(-1.954,-2.39295984553393E-16,0.));
#16772=CARTESIAN_POINT('Ctrl Pts',(-1.95467666345581,-0.00169153748172557,
6.52586969212423));
#16773=CARTESIAN_POINT('Ctrl Pts',(-1.94989845242835,0.519322657074601,
6.49612723996228));
#16774=CARTESIAN_POINT('Ctrl Pts',(-1.7351643372623,1.04378980187726,6.46638478780033));
#16775=CARTESIAN_POINT('Ctrl Pts',(-1.36233982826997,1.40523012754949,6.43664233563838));
#16776=CARTESIAN_POINT('Ctrl Pts',(-0.898073529048792,1.85532007158963,
6.39960502220555));
#16777=CARTESIAN_POINT('Ctrl Pts',(-0.188657797713761,2.05260571068844,
6.36256770877271));
#16778=CARTESIAN_POINT('Ctrl Pts',(0.441334197613014,1.90680041588618,6.32553039533987));
#16779=CARTESIAN_POINT('Ctrl Pts',(1.07132619293978,1.76099512108392,6.28849308190704));
#16780=CARTESIAN_POINT('Ctrl Pts',(1.62189445225829,1.2720988923806,6.2514557684742));
#16781=CARTESIAN_POINT('Ctrl Pts',(1.84119904752624,0.663781270447278,6.21441845504137));
#16782=CARTESIAN_POINT('Ctrl Pts',(2.06050364279419,0.055463648513944,6.17738114160853));
#16783=CARTESIAN_POINT('Ctrl Pts',(1.94854457401157,-0.672275366649399,
6.14034382817569));
#16784=CARTESIAN_POINT('Ctrl Pts',(1.556526550614,-1.18653430832568,6.10330651474286));
#16785=CARTESIAN_POINT('Ctrl Pts',(1.16450852721644,-1.70079325000195,6.06626920131002));
#16786=CARTESIAN_POINT('Ctrl Pts',(0.492431549203928,-2.00157211819116,
6.02923188787718));
#16787=CARTESIAN_POINT('Ctrl Pts',(-0.152249713101387,-1.9512713582857,
5.99219457444435));
#16788=CARTESIAN_POINT('Ctrl Pts',(-0.796930975406703,-1.90097059838025,
5.95515726101152));
#16789=CARTESIAN_POINT('Ctrl Pts',(-1.41421652200483,-1.49959021038012,
5.91811994757868));
#16790=CARTESIAN_POINT('Ctrl Pts',(-1.72172624414277,-0.930748421541415,
5.88108263414585));
#16791=CARTESIAN_POINT('Ctrl Pts',(-1.87453175193852,-0.648083672620247,
5.86267832013864));
#16792=CARTESIAN_POINT('Ctrl Pts',(-1.95084670040156,-0.324068969295429,
5.84427400613143));
#16793=CARTESIAN_POINT('Ctrl Pts',(-1.95079807093469,-3.26933958413878E-5,
5.82586969212423));
#16794=CARTESIAN_POINT('Ctrl Pts',(-1.95085192255358,0.000383174536113729,
5.72413030787576));
#16795=CARTESIAN_POINT('Ctrl Pts',(-1.95023983077328,-0.349414785416059,
5.7439992017633));
#16796=CARTESIAN_POINT('Ctrl Pts',(-1.86056894683247,-0.699505544060014,
5.76386809565083));
#16797=CARTESIAN_POINT('Ctrl Pts',(-1.68370318859703,-0.997916657928721,
5.78373698953837));
#16798=CARTESIAN_POINT('Ctrl Pts',(-1.35367274197203,-1.55475001092207,
5.82081222665079));
#16799=CARTESIAN_POINT('Ctrl Pts',(-0.7200355266604,-1.9316382687018,5.85788746376322));
#16800=CARTESIAN_POINT('Ctrl Pts',(-0.0731991044283191,-1.95584662548515,
5.89496270087565));
#16801=CARTESIAN_POINT('Ctrl Pts',(0.573637317803748,-1.9800549822685,5.93203793798808));
#16802=CARTESIAN_POINT('Ctrl Pts',(1.23367294695625,-1.65158343805548,5.9691131751005));
#16803=CARTESIAN_POINT('Ctrl Pts',(1.60440177887889,-1.12097662310535,6.00618841221292));
#16804=CARTESIAN_POINT('Ctrl Pts',(1.97513061080152,-0.590369808155209,
6.04326364932535));
#16805=CARTESIAN_POINT('Ctrl Pts',(2.05655264549427,0.142372277532039,6.08033888643777));
#16806=CARTESIAN_POINT('Ctrl Pts',(1.81135015364285,0.741420988743503,6.1174141235502));
#16807=CARTESIAN_POINT('Ctrl Pts',(1.56614766179142,1.34046969995497,6.15448936066263));
#16808=CARTESIAN_POINT('Ctrl Pts',(0.994320643395809,1.80582503669066,6.19156459777505));
#16809=CARTESIAN_POINT('Ctrl Pts',(0.357948800551169,1.92420559652088,6.22863983488748));
#16810=CARTESIAN_POINT('Ctrl Pts',(-0.278423042293462,2.04258615635109,
6.2657150719999));
#16811=CARTESIAN_POINT('Ctrl Pts',(-0.97933970958712,1.81399193927586,6.30279030911233));
#16812=CARTESIAN_POINT('Ctrl Pts',(-1.42356034057997,1.34319300038089,6.33986554622475));
#16813=CARTESIAN_POINT('Ctrl Pts',(-1.76010254058954,0.986515035416152,
6.36795380010842));
#16814=CARTESIAN_POINT('Ctrl Pts',(-1.9493114895094,0.49082125388787,6.3960420539921));
#16815=CARTESIAN_POINT('Ctrl Pts',(-1.95381346134878,-0.0017935399644829,
6.42413030787577));
#16816=CARTESIAN_POINT('Origin',(0.,0.,-1.2940562256037));
#16817=CARTESIAN_POINT('',(-1.55603866428123,-0.00134656425434549,6.75594377439631));
#16818=CARTESIAN_POINT('',(-1.55791343064937,0.000503462391539915,6.89405622560371));
#16819=CARTESIAN_POINT('',(-1.5555,-9.09151186476045E-14,-1.2940562256037));
#16820=CARTESIAN_POINT('',(-1.54730100999696,0.15949869736893,7.4445));
#16821=CARTESIAN_POINT('Ctrl Pts',(-1.55603866428123,-0.00134656425434554,
6.7559437743963));
#16822=CARTESIAN_POINT('Ctrl Pts',(-1.55697159855378,-0.103073339358787,
6.76323863566719));
#16823=CARTESIAN_POINT('Ctrl Pts',(-1.50153911503434,-0.720280229157285,
6.80757081037091));
#16824=CARTESIAN_POINT('Ctrl Pts',(-0.676946582872774,-1.70937536089767,
6.88894029850746));
#16825=CARTESIAN_POINT('Ctrl Pts',(1.06890459630572,-1.49565296874813,7.00005223880597));
#16826=CARTESIAN_POINT('Ctrl Pts',(1.83584092749207,0.0856835708872964,
7.11116417910447));
#16827=CARTESIAN_POINT('Ctrl Pts',(0.924965623038614,1.59014055343882,7.22227611940298));
#16828=CARTESIAN_POINT('Ctrl Pts',(-0.835858495286665,1.63675999125994,
7.33338805970149));
#16829=CARTESIAN_POINT('Ctrl Pts',(-1.49427628245053,0.673892957891604,
7.40746268656716));
#16830=CARTESIAN_POINT('Ctrl Pts',(-1.54730100999696,0.159498697368912,
7.4445));
#16831=CARTESIAN_POINT('',(-0.352169241380506,1.51510959188617,7.4445));
#16832=CARTESIAN_POINT('Origin',(0.,0.,7.4445));
#16833=CARTESIAN_POINT('Ctrl Pts',(-1.55791343064937,0.000503462391539858,
6.8940562256037));
#16834=CARTESIAN_POINT('Ctrl Pts',(-1.55587997194015,-0.488621135891717,
6.9292365352861));
#16835=CARTESIAN_POINT('Ctrl Pts',(-1.04365545248604,-1.49691459517969,
7.00149208208092));
#16836=CARTESIAN_POINT('Ctrl Pts',(0.672826183539381,-1.71093187207897,
7.11082286598819));
#16837=CARTESIAN_POINT('Ctrl Pts',(1.80435891657647,-0.361603954366771,
7.22204857732544));
#16838=CARTESIAN_POINT('Ctrl Pts',(1.27791236939833,1.32169962363241,7.33327428866273));
#16839=CARTESIAN_POINT('Ctrl Pts',(0.152038852759137,1.63230677878407,7.40742476288758));
#16840=CARTESIAN_POINT('Ctrl Pts',(-0.352169241380528,1.51510959188617,
7.44450000000001));
#16841=CARTESIAN_POINT('Origin',(0.,0.,-1.2940562256037));
#16842=CARTESIAN_POINT('',(-1.5529510743802,-2.6025883987463E-5,6.0559437743963));
#16843=CARTESIAN_POINT('',(-1.55535150415969,-0.0014277642860383,6.1940562256037));
#16844=CARTESIAN_POINT('',(-1.5555,-9.09151186476045E-14,-1.2940562256037));
#16845=CARTESIAN_POINT('Ctrl Pts',(-1.5529510743802,-2.60258839871949E-5,
6.0559437743963));
#16846=CARTESIAN_POINT('Ctrl Pts',(-1.55298978632273,-0.257978138044578,
6.07434808840351));
#16847=CARTESIAN_POINT('Ctrl Pts',(-1.36998122495718,-1.03498796260698,
6.12978971584355));
#16848=CARTESIAN_POINT('Ctrl Pts',(-0.143008426055117,-1.83280806515592,
6.2222686567164));
#16849=CARTESIAN_POINT('Ctrl Pts',(1.4620310918033,-1.11449456034272,6.33338059701493));
#16850=CARTESIAN_POINT('Ctrl Pts',(1.72940928754233,0.623475815429911,6.44449253731343));
#16851=CARTESIAN_POINT('Ctrl Pts',(0.414554230167772,1.79104708014026,6.55560447761194));
#16852=CARTESIAN_POINT('Ctrl Pts',(-1.16842639544942,1.35082658514471,6.65942155663957));
#16853=CARTESIAN_POINT('Ctrl Pts',(-1.55223492464296,0.413411664830818,
6.72620132223435));
#16854=CARTESIAN_POINT('Ctrl Pts',(-1.55603866428123,-0.00134656425434554,
6.7559437743963));
#16855=CARTESIAN_POINT('Ctrl Pts',(-1.55535150415969,-0.00142776428603842,
6.1940562256037));
#16856=CARTESIAN_POINT('Ctrl Pts',(-1.55649817143771,-0.126898399140172,
6.20304320883246));
#16857=CARTESIAN_POINT('Ctrl Pts',(-1.48522496230459,-0.768704224613979,
6.24910542917363));
#16858=CARTESIAN_POINT('Ctrl Pts',(-0.59667036110871,-1.73952595846347,
6.33224288662724));
#16859=CARTESIAN_POINT('Ctrl Pts',(1.13899278941852,-1.44381691390763,6.44346859796452));
#16860=CARTESIAN_POINT('Ctrl Pts',(1.83065601360088,0.17532136832598,6.5546943093018));
#16861=CARTESIAN_POINT('Ctrl Pts',(0.844193344579619,1.63380261073593,6.66592002063907));
#16862=CARTESIAN_POINT('Ctrl Pts',(-0.915934603694247,1.5945880622222,6.77714573197635));
#16863=CARTESIAN_POINT('Ctrl Pts',(-1.5455164129256,0.568558209121068,6.85319113363123));
#16864=CARTESIAN_POINT('Ctrl Pts',(-1.55802295943751,0.0268493253573782,
6.89216129817368));
#16865=CARTESIAN_POINT('Ctrl Pts',(-1.55791343064937,0.000503462391539858,
6.8940562256037));
#16866=CARTESIAN_POINT('Origin',(0.,0.,-1.2940562256037));
#16867=CARTESIAN_POINT('',(-1.555966115901,0.00138046790836748,5.3559437743963));
#16868=CARTESIAN_POINT('',(-1.55299394346576,0.000305029677950264,5.49405622560371));
#16869=CARTESIAN_POINT('',(-1.5555,-9.09151186476045E-14,-1.2940562256037));
#16870=CARTESIAN_POINT('Ctrl Pts',(-1.555966115901,0.00138046790836748,
5.3559437743963));
#16871=CARTESIAN_POINT('Ctrl Pts',(-1.55217699502656,-0.410255201607083,
5.38545754113982));
#16872=CARTESIAN_POINT('Ctrl Pts',(-1.17320681553292,-1.34462621114732,
5.45200862131617));
#16873=CARTESIAN_POINT('Ctrl Pts',(0.403496653242899,-1.79354886637635,
5.55559701492538));
#16874=CARTESIAN_POINT('Ctrl Pts',(1.72554797232085,-0.634122566945669,
5.66670895522387));
#16875=CARTESIAN_POINT('Ctrl Pts',(1.46886056527041,1.10547479200108,5.77782089552239));
#16876=CARTESIAN_POINT('Ctrl Pts',(-0.131715923640121,1.83365183655613,
5.88893283582089));
#16877=CARTESIAN_POINT('Ctrl Pts',(-1.36662941760285,1.04145067599478,5.9816404621122));
#16878=CARTESIAN_POINT('Ctrl Pts',(-1.55291188141693,0.261131306893961,
6.03731077497067));
#16879=CARTESIAN_POINT('Ctrl Pts',(-1.5529510743802,-2.60258839871949E-5,
6.0559437743963));
#16880=CARTESIAN_POINT('Ctrl Pts',(-1.55299394346576,0.000305029677950229,
5.49405622560371));
#16881=CARTESIAN_POINT('Ctrl Pts',(-1.55250668207154,-0.278154912341265,
5.51392511949124));
#16882=CARTESIAN_POINT('Ctrl Pts',(-1.34792243677793,-1.07688746067556,
5.5708692504912));
#16883=CARTESIAN_POINT('Ctrl Pts',(-0.0687781849042931,-1.83772416168987,
5.66488861860358));
#16884=CARTESIAN_POINT('Ctrl Pts',(1.50750444735784,-1.05327561457109,5.77611432994086));
#16885=CARTESIAN_POINT('Ctrl Pts',(1.70195476716013,0.696642984640571,5.88734004127814));
#16886=CARTESIAN_POINT('Ctrl Pts',(0.336330007005007,1.80799440678846,5.99856575261541));
#16887=CARTESIAN_POINT('Ctrl Pts',(-1.20233240386818,1.30618107352199,6.10080448072394));
#16888=CARTESIAN_POINT('Ctrl Pts',(-1.55176766731418,0.390722855896857,
6.16596797172003));
#16889=CARTESIAN_POINT('Ctrl Pts',(-1.55535150415969,-0.00142776428603842,
6.1940562256037));
#16890=CARTESIAN_POINT('Origin',(0.,0.,-1.2940562256037));
#16891=CARTESIAN_POINT('',(-1.55745403705147,-0.000857197650203868,4.6559437743963));
#16892=CARTESIAN_POINT('',(-1.55647172954169,0.00128913277620515,4.7940562256037));
#16893=CARTESIAN_POINT('',(-1.5555,-9.09151186476045E-14,-1.2940562256037));
#16894=CARTESIAN_POINT('Ctrl Pts',(-1.55745403705147,-0.000857197650203714,
4.6559437743963));
#16895=CARTESIAN_POINT('Ctrl Pts',(-1.55778482013651,-0.0507465481586787,
4.6595296804433));
#16896=CARTESIAN_POINT('Ctrl Pts',(-1.5329809661149,-0.615588902391355,
4.70015289992314));
#16897=CARTESIAN_POINT('Ctrl Pts',(-0.843859631129698,-1.63325682938675,
4.77781343283583));
#16898=CARTESIAN_POINT('Ctrl Pts',(0.914157055608714,-1.59497455450745,
4.88892537313433));
#16899=CARTESIAN_POINT('Ctrl Pts',(1.83579319504673,-0.0974181938582904,
5.00003731343284));
#16900=CARTESIAN_POINT('Ctrl Pts',(1.07782545884778,1.48926801121999,5.11114925373134));
#16901=CARTESIAN_POINT('Ctrl Pts',(-0.666266304296033,1.713393176152,5.22226119402985));
#16902=CARTESIAN_POINT('Ctrl Pts',(-1.49942664147989,0.726761727184559,
5.30385936758484));
#16903=CARTESIAN_POINT('Ctrl Pts',(-1.55693202540547,0.106313199995716,
5.34842022770699));
#16904=CARTESIAN_POINT('Ctrl Pts',(-1.555966115901,0.00138046790836748,
5.3559437743963));
#16905=CARTESIAN_POINT('Ctrl Pts',(-1.55647172954169,0.00128913277620508,
4.7940562256037));
#16906=CARTESIAN_POINT('Ctrl Pts',(-1.55265159250384,-0.427240132487249,
4.82480703015002));
#16907=CARTESIAN_POINT('Ctrl Pts',(-1.14657973682021,-1.37879177584745,
4.89263307180876));
#16908=CARTESIAN_POINT('Ctrl Pts',(0.464983542380115,-1.77925562259896,
4.99753435057992));
#16909=CARTESIAN_POINT('Ctrl Pts',(1.74748619395055,-0.572933012383953,
5.1087600619172));
#16910=CARTESIAN_POINT('Ctrl Pts',(1.42817970701863,1.15856074316792,5.21998577325448));
#16911=CARTESIAN_POINT('Ctrl Pts',(-0.20024807751692,1.82807576816643,5.33121148459175));
#16912=CARTESIAN_POINT('Ctrl Pts',(-1.38701509520349,1.00164745002229,5.4225683020415));
#16913=CARTESIAN_POINT('Ctrl Pts',(-1.55341590891771,0.24144967335499,5.47684988237881));
#16914=CARTESIAN_POINT('Ctrl Pts',(-1.55299394346576,0.000305029677950229,
5.49405622560371));
#16915=CARTESIAN_POINT('Origin',(0.,0.,-1.2940562256037));
#16916=CARTESIAN_POINT('',(-1.55339080467029,-0.000825238370695906,3.9559437743963));
#16917=CARTESIAN_POINT('',(-1.55714699541918,-0.00104284411826,4.0940562256037));
#16918=CARTESIAN_POINT('',(-1.5555,-9.09151186476045E-14,-1.2940562256037));
#16919=CARTESIAN_POINT('Ctrl Pts',(-1.55339080467029,-0.000825238370696021,
3.9559437743963));
#16920=CARTESIAN_POINT('Ctrl Pts',(-1.55438190323133,-0.206647724104582,
3.97063913317962));
#16921=CARTESIAN_POINT('Ctrl Pts',(-1.42057875865067,-0.929976336606789,
4.02237180539578));
#16922=CARTESIAN_POINT('Ctrl Pts',(-0.325039216866852,-1.80941329116195,
4.11114179104478));
#16923=CARTESIAN_POINT('Ctrl Pts',(1.34361459616473,-1.25472178898058,4.22225373134328));
#16924=CARTESIAN_POINT('Ctrl Pts',(1.78296857449566,0.447939743012656,4.3333656716418));
#16925=CARTESIAN_POINT('Ctrl Pts',(0.591048986302979,1.74077225568864,4.44447761194029));
#16926=CARTESIAN_POINT('Ctrl Pts',(-1.08571442614287,1.45061399985919,4.5520036461918));
#16927=CARTESIAN_POINT('Ctrl Pts',(-1.55436830095327,0.464539543423835,
4.62249236701046));
#16928=CARTESIAN_POINT('Ctrl Pts',(-1.55745403705147,-0.000857197650203714,
4.6559437743963));
#16929=CARTESIAN_POINT('Ctrl Pts',(-1.55714699541918,-0.00104284411826003,
4.0940562256037));
#16930=CARTESIAN_POINT('Ctrl Pts',(-1.55763619195644,-0.0644821423710283,
4.09861370369637));
#16931=CARTESIAN_POINT('Ctrl Pts',(-1.52529338404343,-0.643499375005814,
4.14024641890147));
#16932=CARTESIAN_POINT('Ctrl Pts',(-0.799431294618187,-1.65616118233816,
4.21895437121899));
#16933=CARTESIAN_POINT('Ctrl Pts',(0.959104426053338,-1.56910132141185,
4.33018008255627));
#16934=CARTESIAN_POINT('Ctrl Pts',(1.83849028118038,-0.0437463405035559,
4.44140579389354));
#16935=CARTESIAN_POINT('Ctrl Pts',(1.0326493363287,1.52170812080878,4.55263150523082));
#16936=CARTESIAN_POINT('Ctrl Pts',(-0.719755403894915,1.69230978744094,
4.6638572165681));
#16937=CARTESIAN_POINT('Ctrl Pts',(-1.51031879937117,0.693384867678679,
4.74433212335906));
#16938=CARTESIAN_POINT('Ctrl Pts',(-1.55725740651651,0.0894235565985826,
4.78773179303759));
#16939=CARTESIAN_POINT('Ctrl Pts',(-1.55647172954169,0.00128913277620508,
4.7940562256037));
#16940=CARTESIAN_POINT('Origin',(0.,0.,-1.2940562256037));
#16941=CARTESIAN_POINT('',(-1.55444809594431,0.00131769509984214,3.2559437743963));
#16942=CARTESIAN_POINT('',(-1.55323130759427,-0.000686532414708174,3.3940562256037));
#16943=CARTESIAN_POINT('',(-1.5555,-9.09151186476045E-14,-1.2940562256037));
#16944=CARTESIAN_POINT('Ctrl Pts',(-1.55444809594431,0.00131769509984224,
3.2559437743963));
#16945=CARTESIAN_POINT('Ctrl Pts',(-1.55154267442328,-0.359485027434377,
3.28174858591594));
#16946=CARTESIAN_POINT('Ctrl Pts',(-1.24686166172698,-1.24256912580371,
3.34459071086842));
#16947=CARTESIAN_POINT('Ctrl Pts',(0.222653802667342,-1.82484307132901,
3.44447014925373));
#16948=CARTESIAN_POINT('Ctrl Pts',(1.65372145106143,-0.803014516107455,
3.55558208955224));
#16949=CARTESIAN_POINT('Ctrl Pts',(1.57176630825256,0.953508061332994,3.66669402985075));
#16950=CARTESIAN_POINT('Ctrl Pts',(0.0517707715753711,1.83764706567811,
3.77780597014925));
#16951=CARTESIAN_POINT('Ctrl Pts',(-1.30829594910608,1.14591637592306,3.87422255166444));
#16952=CARTESIAN_POINT('Ctrl Pts',(-1.55188399701554,0.312095099942876,
3.93360181974679));
#16953=CARTESIAN_POINT('Ctrl Pts',(-1.55339080467029,-0.000825238370696021,
3.9559437743963));
#16954=CARTESIAN_POINT('Ctrl Pts',(-1.55323130759427,-0.000686532414707983,
3.3940562256037));
#16955=CARTESIAN_POINT('Ctrl Pts',(-1.55409097737417,-0.216984975064148,
3.40949561435515));
#16956=CARTESIAN_POINT('Ctrl Pts',(-1.4109189051218,-0.95160176519996,3.46201024021903));
#16957=CARTESIAN_POINT('Ctrl Pts',(-0.286969261786828,-1.81648256240041,
3.55160010319533));
#16958=CARTESIAN_POINT('Ctrl Pts',(1.37145934362907,-1.22517734450477,3.66282581453261));
#16959=CARTESIAN_POINT('Ctrl Pts',(1.77275862659963,0.489169815626649,3.77405152586988));
#16960=CARTESIAN_POINT('Ctrl Pts',(0.549083125265984,1.75512620009375,3.88527723720716));
#16961=CARTESIAN_POINT('Ctrl Pts',(-1.10713858120128,1.42631885494224,3.99194547045177));
#16962=CARTESIAN_POINT('Ctrl Pts',(-1.5536565617213,0.451598676262059,4.06153846658395));
#16963=CARTESIAN_POINT('Ctrl Pts',(-1.55714699541918,-0.00104284411826003,
4.0940562256037));
#16964=CARTESIAN_POINT('Origin',(0.,0.,-1.2940562256037));
#16965=CARTESIAN_POINT('',(-1.55804749425921,3.19249239839854E-5,2.5559437743963));
#16966=CARTESIAN_POINT('',(-1.55463050379685,0.00136373510819555,2.6940562256037));
#16967=CARTESIAN_POINT('',(-1.5555,-9.09151186476045E-14,-1.2940562256037));
#16968=CARTESIAN_POINT('Ctrl Pts',(-1.55804749425921,3.19249239839832E-5,
2.5559437743963));
#16969=CARTESIAN_POINT('Ctrl Pts',(-1.55789240629065,-0.513022302446059,
2.59285803865226));
#16970=CARTESIAN_POINT('Ctrl Pts',(-1.00056267955874,-1.54112970888597,
2.66680961634105));
#16971=CARTESIAN_POINT('Ctrl Pts',(0.750568915726592,-1.67817557333754,
2.77779850746269));
#16972=CARTESIAN_POINT('Ctrl Pts',(1.81693142975936,-0.279977017554228,
2.8889104477612));
#16973=CARTESIAN_POINT('Ctrl Pts',(1.22094708256035,1.37437810371544,3.0000223880597));
#16974=CARTESIAN_POINT('Ctrl Pts',(-0.492106140687917,1.77128724302598,
3.11113432835821));
#16975=CARTESIAN_POINT('Ctrl Pts',(-1.46164337385231,0.831798954515017,
3.19644145713707));
#16976=CARTESIAN_POINT('Ctrl Pts',(-1.55571278849084,0.158370470628406,
3.2447112724831));
#16977=CARTESIAN_POINT('Ctrl Pts',(-1.55444809594431,0.00131769509984224,
3.2559437743963));
#16978=CARTESIAN_POINT('Ctrl Pts',(-1.55463050379685,0.0013637351081955,
2.6940562256037));
#16979=CARTESIAN_POINT('Ctrl Pts',(-1.55154239698677,-0.366550683268523,
2.72037752501393));
#16980=CARTESIAN_POINT('Ctrl Pts',(-1.23694887232287,-1.2574453593796,2.78377406153659));
#16981=CARTESIAN_POINT('Ctrl Pts',(0.249957593646744,-1.82194441691009,
2.88424583517168));
#16982=CARTESIAN_POINT('Ctrl Pts',(1.6668940398915,-0.776804039943688,2.99547154650895));
#16983=CARTESIAN_POINT('Ctrl Pts',(1.55589501744036,0.980383063583733,3.10669725784622));
#16984=CARTESIAN_POINT('Ctrl Pts',(0.0187062518377651,1.83891553174339,
3.2179229691835));
#16985=CARTESIAN_POINT('Ctrl Pts',(-1.31986995326957,1.12664004660162,3.31370929176933));
#16986=CARTESIAN_POINT('Ctrl Pts',(-1.55202661709144,0.302421341945843,
3.37242037724273));
#16987=CARTESIAN_POINT('Ctrl Pts',(-1.55323130759427,-0.000686532414707983,
3.3940562256037));
#16988=CARTESIAN_POINT('Origin',(0.,0.,-1.2940562256037));
#16989=CARTESIAN_POINT('',(-1.55454086388192,-0.001338238080313,1.8559437743963));
#16990=CARTESIAN_POINT('',(-1.55805913879558,-3.33498767488005E-5,1.9940562256037));
#16991=CARTESIAN_POINT('',(-1.5555,-9.09151186476045E-14,-1.2940562256037));
#16992=CARTESIAN_POINT('Ctrl Pts',(-1.55454086388192,-0.00133823808031298,
1.8559437743963));
#16993=CARTESIAN_POINT('Ctrl Pts',(-1.55580261226994,-0.154926887448841,
1.86693017795574));
#16994=CARTESIAN_POINT('Ctrl Pts',(-1.46434456543453,-0.824823376066396,
1.91495389494802));
#16995=CARTESIAN_POINT('Ctrl Pts',(-0.503833422351614,-1.76798718278107,
2.00001492537314));
#16996=CARTESIAN_POINT('Ctrl Pts',(1.211812440791,-1.38243900779253,2.11112686567164));
#16997=CARTESIAN_POINT('Ctrl Pts',(1.81874690762903,0.2679303086893,2.22223880597015));
#16998=CARTESIAN_POINT('Ctrl Pts',(0.761673489280804,1.67316479305249,2.33335074626865));
#16999=CARTESIAN_POINT('Ctrl Pts',(-0.99227021626331,1.54758740541246,2.44446268656716));
#17000=CARTESIAN_POINT('Ctrl Pts',(-1.5572711215541,0.518216278848874,2.51866036260971));
#17001=CARTESIAN_POINT('Ctrl Pts',(-1.55804801122595,0.00174212832754369,
2.55582072521942));
#17002=CARTESIAN_POINT('Ctrl Pts',(-1.55804749425921,3.19249239839832E-5,
2.5559437743963));
#17003=CARTESIAN_POINT('Ctrl Pts',(-1.55805913879558,-3.33498767486382E-5,
1.9940562256037));
#17004=CARTESIAN_POINT('Ctrl Pts',(-1.5580596990309,-0.00181195213168648,
1.99418419856029));
#17005=CARTESIAN_POINT('Ctrl Pts',(-1.5572509939767,-0.518871555499298,
2.0313874086293));
#17006=CARTESIAN_POINT('Ctrl Pts',(-0.990825815880477,-1.5492657736205,
2.10566585581074));
#17007=CARTESIAN_POINT('Ctrl Pts',(0.765574959497512,-1.6720811124538,2.21689156714802));
#17008=CARTESIAN_POINT('Ctrl Pts',(1.82022199392772,-0.262206313316451,
2.32811727848529));
#17009=CARTESIAN_POINT('Ctrl Pts',(1.20638759997596,1.38801628675575,2.43934298982257));
#17010=CARTESIAN_POINT('Ctrl Pts',(-0.513265374585843,1.76593287340023,
2.55056870115984));
#17011=CARTESIAN_POINT('Ctrl Pts',(-1.46682634638563,0.818764115677731,
2.63547311308689));
#17012=CARTESIAN_POINT('Ctrl Pts',(-1.55589219334096,0.151680354105525,
2.68330228790151));
#17013=CARTESIAN_POINT('Ctrl Pts',(-1.55463050379685,0.0013637351081955,
2.6940562256037));
#17014=CARTESIAN_POINT('Origin',(0.,0.,-1.2940562256037));
#17015=CARTESIAN_POINT('',(-1.55333683422467,0.00078011305757314,1.1559437743963));
#17016=CARTESIAN_POINT('',(-1.55453190133567,-0.00134444967022529,1.2940562256037));
#17017=CARTESIAN_POINT('',(-1.5555,-9.09151186476045E-14,-1.2940562256037));
#17018=CARTESIAN_POINT('Ctrl Pts',(-1.55333683422467,0.000780113057573043,
1.1559437743963));
#17019=CARTESIAN_POINT('Ctrl Pts',(-1.55193443781686,-0.308720927367064,
1.17803963069206));
#17020=CARTESIAN_POINT('Ctrl Pts',(-1.31240187276934,-1.13901289380036,
1.23717280042066));
#17021=CARTESIAN_POINT('Ctrl Pts',(0.0395921340189295,-1.83794780075079,
1.33334328358209));
#17022=CARTESIAN_POINT('Ctrl Pts',(1.56541283438613,-0.96390406493211,1.44445522388059));
#17023=CARTESIAN_POINT('Ctrl Pts',(1.65900671048959,0.792038431388639,1.55556716417911));
#17024=CARTESIAN_POINT('Ctrl Pts',(0.234741865039883,1.82332721494359,1.66667910447761));
#17025=CARTESIAN_POINT('Ctrl Pts',(-1.24223016373737,1.24939407250205,1.76680464121668));
#17026=CARTESIAN_POINT('Ctrl Pts',(-1.55154901187489,0.362850464858491,
1.8298928645229));
#17027=CARTESIAN_POINT('Ctrl Pts',(-1.55454086388192,-0.00133823808031298,
1.8559437743963));
#17028=CARTESIAN_POINT('Ctrl Pts',(-1.55453190133567,-0.00134444967022513,
1.2940562256037));
#17029=CARTESIAN_POINT('Ctrl Pts',(-1.55579946924303,-0.155263418355649,
1.30506610921907));
#17030=CARTESIAN_POINT('Ctrl Pts',(-1.46404280977096,-0.826019057429759,
1.35315122994686));
#17031=CARTESIAN_POINT('Ctrl Pts',(-0.501082205369057,-1.76942810040879,
1.43831158778708));
#17032=CARTESIAN_POINT('Ctrl Pts',(1.21592516185098,-1.37966899434435,1.54953729912436));
#17033=CARTESIAN_POINT('Ctrl Pts',(1.8183716526183,0.274745208061178,1.66076301046163));
#17034=CARTESIAN_POINT('Ctrl Pts',(0.754032712405612,1.67731773070425,1.77198872179891));
#17035=CARTESIAN_POINT('Ctrl Pts',(-0.999460041113845,1.5425554247787,1.8830864601796));
#17036=CARTESIAN_POINT('Ctrl Pts',(-1.5578973924169,0.513469573665662,1.95710896144786));
#17037=CARTESIAN_POINT('Ctrl Pts',(-1.55805913879558,-3.33498767486382E-5,
1.9940562256037));
#17038=CARTESIAN_POINT('Origin',(0.,0.,-1.2940562256037));
#17039=CARTESIAN_POINT('',(-1.55735958542387,0.00101297198046619,0.455943774396298));
#17040=CARTESIAN_POINT('',(-1.55327638232574,0.000749985450956003,0.594056225603703));
#17041=CARTESIAN_POINT('',(-1.5555,-9.09151186476045E-14,-1.2940562256037));
#17042=CARTESIAN_POINT('Ctrl Pts',(-1.55735958542387,0.00101297198046621,
0.455943774396298));
#17043=CARTESIAN_POINT('Ctrl Pts',(-1.55415428451722,-0.460990851268869,
0.489149083428377));
#17044=CARTESIAN_POINT('Ctrl Pts',(-1.09150079880486,-1.44424863810505,
0.559391705893293));
#17045=CARTESIAN_POINT('Ctrl Pts',(0.579516952736672,-1.74455562530747,
0.666671641791043));
#17046=CARTESIAN_POINT('Ctrl Pts',(1.77995215483547,-0.45979539180552,0.777783582089551));
#17047=CARTESIAN_POINT('Ctrl Pts',(1.35190460952174,1.24581651128198,0.888895522388059));
#17048=CARTESIAN_POINT('Ctrl Pts',(-0.313043761712607,1.81151378121076,
1.00000746268657));
#17049=CARTESIAN_POINT('Ctrl Pts',(-1.41743746237044,0.936955068058493,
1.08902354668931));
#17050=CARTESIAN_POINT('Ctrl Pts',(-1.55428514985164,0.21006806585223,1.14100231725922));
#17051=CARTESIAN_POINT('Ctrl Pts',(-1.55333683422467,0.000780113057573043,
1.1559437743963));
#17052=CARTESIAN_POINT('Ctrl Pts',(-1.55327638232574,0.000749985450955847,
0.594056225603703));
#17053=CARTESIAN_POINT('Ctrl Pts',(-1.55196556188379,-0.305924499715954,
0.61594801987785));
#17054=CARTESIAN_POINT('Ctrl Pts',(-1.3156705723219,-1.13385132195631,0.674915051264423));
#17055=CARTESIAN_POINT('Ctrl Pts',(0.0313843551128396,-1.83872969125081,
0.770957319763422));
#17056=CARTESIAN_POINT('Ctrl Pts',(1.56261245507102,-0.969643437172017,
0.882183031100698));
#17057=CARTESIAN_POINT('Ctrl Pts',(1.66150197094076,0.788277540412492,0.993408742437974));
#17058=CARTESIAN_POINT('Ctrl Pts',(0.237394066880885,1.82362194812979,1.10463445377525));
#17059=CARTESIAN_POINT('Ctrl Pts',(-1.24180780125352,1.25035520807598,1.20485028149716));
#17060=CARTESIAN_POINT('Ctrl Pts',(-1.55153099717163,0.363051076099792,
1.26799087210664));
#17061=CARTESIAN_POINT('Ctrl Pts',(-1.55453190133567,-0.00134444967022513,
1.2940562256037));
#17062=CARTESIAN_POINT('Origin',(0.,0.,7.5));
#17063=CARTESIAN_POINT('',(-1.90714972453263,0.000559583190138325,7.09553262944276));
#17064=CARTESIAN_POINT('Ctrl Pts',(-0.352169241380463,1.51510959188618,
7.4445));
#17065=CARTESIAN_POINT('Ctrl Pts',(-0.294581668876612,1.53128067531421,
7.44178679402676));
#17066=CARTESIAN_POINT('Ctrl Pts',(-0.236177221040451,1.54382025621514,
7.43908623010619));
#17067=CARTESIAN_POINT('Ctrl Pts',(-0.17725379571509,1.55288079770358,7.43639376053775));
#17068=CARTESIAN_POINT('Ctrl Pts',(-0.119240420394871,1.56180140255761,
7.43374287514286));
#17069=CARTESIAN_POINT('Ctrl Pts',(-0.0607231436400752,1.56734934022223,
7.4310998360025));
#17070=CARTESIAN_POINT('Ctrl Pts',(-0.00197185718845893,1.56962582506071,
7.42846030289105));
#17071=CARTESIAN_POINT('Ctrl Pts',(0.0296117181373077,1.57084962005681,
7.4270413400413));
#17072=CARTESIAN_POINT('Ctrl Pts',(0.0612630953454002,1.57112724793077,
7.42562339041052));
#17073=CARTESIAN_POINT('Ctrl Pts',(0.0929408476792332,1.57046939552494,
7.42420577971289));
#17074=CARTESIAN_POINT('Ctrl Pts',(0.105200379607973,1.57021480162293,7.42365715355322));
#17075=CARTESIAN_POINT('Ctrl Pts',(0.117460267523568,1.56982005993498,7.42310873898429));
#17076=CARTESIAN_POINT('Ctrl Pts',(0.129708286104984,1.56928654809906,7.42256093565192));
#17077=CARTESIAN_POINT('Ctrl Pts',(0.192428535028528,1.56655451475585,7.41975571771902));
#17078=CARTESIAN_POINT('Ctrl Pts',(0.254912080108278,1.56018641116159,7.41696316059146));
#17079=CARTESIAN_POINT('Ctrl Pts',(0.316835955987319,1.55031158486179,7.41417821827426));
#17080=CARTESIAN_POINT('Ctrl Pts',(0.379261168612821,1.54035681180124,7.41137072901695));
#17081=CARTESIAN_POINT('Ctrl Pts',(0.441118681165113,1.52683817797346,7.40857097836836));
#17082=CARTESIAN_POINT('Ctrl Pts',(0.502077268456636,1.50983552777742,7.40577379678119));
#17083=CARTESIAN_POINT('Ctrl Pts',(0.518104654250298,1.50536514802758,7.40503835473071));
#17084=CARTESIAN_POINT('Ctrl Pts',(0.534069848209942,1.50065364953946,7.40430309027496));
#17085=CARTESIAN_POINT('Ctrl Pts',(0.549966680795085,1.49570190223715,7.40356790945547));
#17086=CARTESIAN_POINT('Ctrl Pts',(0.559908491182372,1.4926051008774,7.40310813054867));
#17087=CARTESIAN_POINT('Ctrl Pts',(0.569821116728089,1.48941503409471,7.4026484967243));
#17088=CARTESIAN_POINT('Ctrl Pts',(0.579694961183896,1.486134869268,7.40218936420725));
#17089=CARTESIAN_POINT('Ctrl Pts',(0.640449229714658,1.46595184779153,7.39936429841276));
#17090=CARTESIAN_POINT('Ctrl Pts',(0.69982505895545,1.44233435228215,7.39655407027566));
#17091=CARTESIAN_POINT('Ctrl Pts',(0.757493396577592,1.41540064986381,7.39375356846506));
#17092=CARTESIAN_POINT('Ctrl Pts',(0.814802366573082,1.38863478825924,7.39097051833992));
#17093=CARTESIAN_POINT('Ctrl Pts',(0.870426121162267,1.35859365369072,7.38819707369729));
#17094=CARTESIAN_POINT('Ctrl Pts',(0.924030095744784,1.32534364884642,7.38542821816778));
#17095=CARTESIAN_POINT('Ctrl Pts',(0.960999915716867,1.30241164235365,7.38351858196539));
#17096=CARTESIAN_POINT('Ctrl Pts',(0.997008764456124,1.27795226352036,7.38161112864094));
#17097=CARTESIAN_POINT('Ctrl Pts',(1.03193962221215,1.25197434532887,7.3797042125328));
#17098=CARTESIAN_POINT('Ctrl Pts',(1.0531065792895,1.23623257674251,7.37854868375383));
#17099=CARTESIAN_POINT('Ctrl Pts',(1.07387756970412,1.21993300461795,7.37739335223873));
#17100=CARTESIAN_POINT('Ctrl Pts',(1.09422502955045,1.2030757852037,7.37623785181303));
#17101=CARTESIAN_POINT('Ctrl Pts',(1.10258166584356,1.19615257942657,7.37576329150589));
#17102=CARTESIAN_POINT('Ctrl Pts',(1.11086633597203,1.18913559341204,7.3752887282991));
#17103=CARTESIAN_POINT('Ctrl Pts',(1.11906690491304,1.18203401934788,7.37481473623418));
#17104=CARTESIAN_POINT('Ctrl Pts',(1.12385025457867,1.17789170773882,7.37453825910173));
#17105=CARTESIAN_POINT('Ctrl Pts',(1.12860592464056,1.17371985114455,7.37426192347451));
#17106=CARTESIAN_POINT('Ctrl Pts',(1.13333360310225,1.16951854601392,7.37398572456616));
#17107=CARTESIAN_POINT('Ctrl Pts',(1.17895537492945,1.12897624060986,7.37132042410681));
#17108=CARTESIAN_POINT('Ctrl Pts',(1.22197272212526,1.08569548753383,7.36866785506909));
#17109=CARTESIAN_POINT('Ctrl Pts',(1.2623504524016,1.0400250384405,7.36602371637222));
#17110=CARTESIAN_POINT('Ctrl Pts',(1.30450707484485,0.992342519733652,7.36326308678831));
#17111=CARTESIAN_POINT('Ctrl Pts',(1.34378698003833,0.942054513171778,7.36051164672689));
#17112=CARTESIAN_POINT('Ctrl Pts',(1.38011608577908,0.889512321374444,7.35776450122604));
#17113=CARTESIAN_POINT('Ctrl Pts',(1.41047885103542,0.845599150293909,7.35546852029652));
#17114=CARTESIAN_POINT('Ctrl Pts',(1.43877996472123,0.800110306074669,7.35317553916464));
#17115=CARTESIAN_POINT('Ctrl Pts',(1.46495451960825,0.753233209535809,7.35088270017959));
#17116=CARTESIAN_POINT('Ctrl Pts',(1.47224608288955,0.740174446270043,7.35024397372845));
#17117=CARTESIAN_POINT('Ctrl Pts',(1.47937249019278,0.727007875170104,7.34960525830843));
#17118=CARTESIAN_POINT('Ctrl Pts',(1.48633203561836,0.713737394565328,7.34896649214163));
#17119=CARTESIAN_POINT('Ctrl Pts',(1.49231636613785,0.702326456460141,7.34841723387359));
#17120=CARTESIAN_POINT('Ctrl Pts',(1.49817791288619,0.690837217360077,7.34786787112171));
#17121=CARTESIAN_POINT('Ctrl Pts',(1.50390644072503,0.679291229674037,7.3473192635151));
#17122=CARTESIAN_POINT('Ctrl Pts',(1.53283760232342,0.620979767295612,7.34454859437159));
#17123=CARTESIAN_POINT('Ctrl Pts',(1.55843652026989,0.561117048195595,7.34179201389979));
#17124=CARTESIAN_POINT('Ctrl Pts',(1.58063784893836,0.500065381838401,7.33904470742869));
#17125=CARTESIAN_POINT('Ctrl Pts',(1.6031119912636,0.438263502347606,7.3362636415941));
#17126=CARTESIAN_POINT('Ctrl Pts',(1.62210502961578,0.375242296860671,7.33349207908152));
#17127=CARTESIAN_POINT('Ctrl Pts',(1.63750518239391,0.311348169568812,7.33072502553951));
#17128=CARTESIAN_POINT('Ctrl Pts',(1.65022992907376,0.258554109936303,7.32843868098962));
#17129=CARTESIAN_POINT('Ctrl Pts',(1.66050103147123,0.20516326683894,7.32615541484386));
#17130=CARTESIAN_POINT('Ctrl Pts',(1.66822949082188,0.151363515297575,7.32387240968315));
#17131=CARTESIAN_POINT('Ctrl Pts',(1.67108031331177,0.13151822211743,7.32303026998087));
#17132=CARTESIAN_POINT('Ctrl Pts',(1.67358492004799,0.111617257557933,7.32218816579018));
#17133=CARTESIAN_POINT('Ctrl Pts',(1.67573795844748,0.091670001678837,7.32134595570008));
#17134=CARTESIAN_POINT('Ctrl Pts',(1.67695445834914,0.0803994944639542,
7.32087009400991));
#17135=CARTESIAN_POINT('Ctrl Pts',(1.67805865914088,0.0691137533863127,
7.3203941797156));
#17136=CARTESIAN_POINT('Ctrl Pts',(1.67904845798992,0.0578298683786967,
7.31991883455417));
#17137=CARTESIAN_POINT('Ctrl Pts',(1.68482856592515,-0.00806440229655341,
7.31714297121365));
#17138=CARTESIAN_POINT('Ctrl Pts',(1.68672581172374,-0.0740201346390124,
7.31438118276366));
#17139=CARTESIAN_POINT('Ctrl Pts',(1.68463949062778,-0.139690992105407,
7.31162863136205));
#17140=CARTESIAN_POINT('Ctrl Pts',(1.68257287237932,-0.204741665606402,
7.30890207456915));
#17141=CARTESIAN_POINT('Ctrl Pts',(1.67659788793627,-0.2695138491763,7.30618458118234));
#17142=CARTESIAN_POINT('Ctrl Pts',(1.6665669476348,-0.3336793478161,7.30347144913232));
#17143=CARTESIAN_POINT('Ctrl Pts',(1.65656393293128,-0.397666213161047,
7.30076587029591));
#17144=CARTESIAN_POINT('Ctrl Pts',(1.64252742158424,-0.461050667219861,
7.29806462854663));
#17145=CARTESIAN_POINT('Ctrl Pts',(1.62468485220914,-0.523589263699737,
7.29536306097687));
#17146=CARTESIAN_POINT('Ctrl Pts',(1.62063291677799,-0.537791386138751,
7.29474955195105));
#17147=CARTESIAN_POINT('Ctrl Pts',(1.61638449230085,-0.551949831001097,
7.29413602612215));
#17148=CARTESIAN_POINT('Ctrl Pts',(1.61194189299792,-0.566061632343824,
7.29352242888019));
#17149=CARTESIAN_POINT('Ctrl Pts',(1.60819661792182,-0.577958401384625,
7.29300514377289));
#17150=CARTESIAN_POINT('Ctrl Pts',(1.60431575784587,-0.589814146380397,
7.2924881495291));
#17151=CARTESIAN_POINT('Ctrl Pts',(1.60030378247776,-0.601620053553602,
7.29197172819479));
#17152=CARTESIAN_POINT('Ctrl Pts',(1.57922949506156,-0.663634661857349,
7.28925904662807));
#17153=CARTESIAN_POINT('Ctrl Pts',(1.55452233752644,-0.724336859414935,
7.28655946062951));
#17154=CARTESIAN_POINT('Ctrl Pts',(1.52646885207918,-0.783492431203164,
7.28386844992972));
#17155=CARTESIAN_POINT('Ctrl Pts',(1.49785765329009,-0.843824036953083,
7.28112394097306));
#17156=CARTESIAN_POINT('Ctrl Pts',(1.46576530908513,-0.902547787676455,
7.27838835166439));
#17157=CARTESIAN_POINT('Ctrl Pts',(1.43044176155356,-0.95940342094092,7.27565688674544));
#17158=CARTESIAN_POINT('Ctrl Pts',(1.40719192683218,-0.996825598744453,
7.27385904614475));
#17159=CARTESIAN_POINT('Ctrl Pts',(1.38254116404519,-1.03343820105651,7.27206299232293));
#17160=CARTESIAN_POINT('Ctrl Pts',(1.35654982896749,-1.06916144614065,7.2702673579332));
#17161=CARTESIAN_POINT('Ctrl Pts',(1.34005703462379,-1.09182962123443,7.26912793863759));
#17162=CARTESIAN_POINT('Ctrl Pts',(1.32302428798857,-1.11413959500617,7.26798868822771));
#17163=CARTESIAN_POINT('Ctrl Pts',(1.30546545072429,-1.13606969941564,7.26684925734159));
#17164=CARTESIAN_POINT('Ctrl Pts',(1.29557863985671,-1.1484178288128,7.26620768082384));
#17165=CARTESIAN_POINT('Ctrl Pts',(1.28552143085819,-1.16064953781435,7.26556582874875));
#17166=CARTESIAN_POINT('Ctrl Pts',(1.27531693894013,-1.17273679271259,7.26492492457875));
#17167=CARTESIAN_POINT('Ctrl Pts',(1.23124484751569,-1.2249403328029,7.26215692913113));
#17168=CARTESIAN_POINT('Ctrl Pts',(1.18437118678711,-1.27452793646465,7.25940270292496));
#17169=CARTESIAN_POINT('Ctrl Pts',(1.1349613540182,-1.32123869434595,7.25665745327404));
#17170=CARTESIAN_POINT('Ctrl Pts',(1.0857776821155,-1.36773564568569,7.25392476930092));
#17171=CARTESIAN_POINT('Ctrl Pts',(1.03408031096501,-1.41138288844598,7.25120097989535));
#17172=CARTESIAN_POINT('Ctrl Pts',(0.980088635865932,-1.45189422149834,
7.24848135788222));
#17173=CARTESIAN_POINT('Ctrl Pts',(0.928612197667789,-1.49051830805181,
7.24588843120928));
#17174=CARTESIAN_POINT('Ctrl Pts',(0.875049469874555,-1.52629233307795,
7.24329929269164));
#17175=CARTESIAN_POINT('Ctrl Pts',(0.819562927233232,-1.55893273310611,
7.24070984551053));
#17176=CARTESIAN_POINT('Ctrl Pts',(0.806531597661789,-1.56659851637287,
7.24010169913812));
#17177=CARTESIAN_POINT('Ctrl Pts',(0.793394057897985,-1.57409127964972,
7.2394935357407));
#17178=CARTESIAN_POINT('Ctrl Pts',(0.78015224431478,-1.58140700410033,7.23888530224817));
#17179=CARTESIAN_POINT('Ctrl Pts',(0.770009447983695,-1.58701060987914,
7.23841941527599));
#17180=CARTESIAN_POINT('Ctrl Pts',(0.759805087672894,-1.59251043302504,
7.23795347189941));
#17181=CARTESIAN_POINT('Ctrl Pts',(0.749553755678445,-1.59789772385032,
7.23748806565584));
#17182=CARTESIAN_POINT('Ctrl Pts',(0.716202490399591,-1.61542451603163,
7.23597393197059));
#17183=CARTESIAN_POINT('Ctrl Pts',(0.682319909404191,-1.63177984026051,
7.23446389597977));
#17184=CARTESIAN_POINT('Ctrl Pts',(0.647945625107734,-1.64691812240344,
7.23295717369848));
#17185=CARTESIAN_POINT('Ctrl Pts',(0.587919642023283,-1.67335329876966,
7.23032606477447));
#17186=CARTESIAN_POINT('Ctrl Pts',(0.52639576498612,-1.69608014520221,7.22770506060276));
#17187=CARTESIAN_POINT('Ctrl Pts',(0.46370862765048,-1.71520377795159,7.22508998649035));
#17188=CARTESIAN_POINT('Ctrl Pts',(0.400150801058184,-1.73459302725791,
7.22243859046197));
#17189=CARTESIAN_POINT('Ctrl Pts',(0.335396320744255,-1.75027834108098,
7.21979329036732));
#17190=CARTESIAN_POINT('Ctrl Pts',(0.269772608446838,-1.76232212244813,
7.21714973513363));
#17191=CARTESIAN_POINT('Ctrl Pts',(0.241062234316718,-1.76759127679625,
7.2159931797189));
#17192=CARTESIAN_POINT('Ctrl Pts',(0.2121852884367,-1.77216281037181,7.21483695828146));
#17193=CARTESIAN_POINT('Ctrl Pts',(0.183168585619119,-1.77603911617646,
7.21368070646147));
#17194=CARTESIAN_POINT('Ctrl Pts',(0.164433789661126,-1.77854187463173,
7.21293416602716));
#17195=CARTESIAN_POINT('Ctrl Pts',(0.145640727943501,-1.78075477785065,
7.21218761292724));
#17196=CARTESIAN_POINT('Ctrl Pts',(0.126796600025785,-1.78267808932064,
7.21144094909238));
#17197=CARTESIAN_POINT('Ctrl Pts',(0.114847127630937,-1.78389770306013,
7.21096747327424));
#17198=CARTESIAN_POINT('Ctrl Pts',(0.102876237812544,-1.78500084411828,
7.21049391856396));
#17199=CARTESIAN_POINT('Ctrl Pts',(0.0909023739078884,-1.78598642534176,
7.21002091434047));
#17200=CARTESIAN_POINT('Ctrl Pts',(0.0223150311249881,-1.79163192104421,
7.20731150465678));
#17201=CARTESIAN_POINT('Ctrl Pts',(-0.0464949765975819,-1.79343822563924,
7.204615131498));
#17202=CARTESIAN_POINT('Ctrl Pts',(-0.115169948787061,-1.79150548386327,
7.201927305065));
#17203=CARTESIAN_POINT('Ctrl Pts',(-0.184810802193317,-1.78954555898233,
7.1992016756161));
#17204=CARTESIAN_POINT('Ctrl Pts',(-0.254313838210283,-1.78374072590431,
7.19648483499498));
#17205=CARTESIAN_POINT('Ctrl Pts',(-0.323317077031426,-1.77414310096439,
7.19377210128489));
#17206=CARTESIAN_POINT('Ctrl Pts',(-0.390207228852162,-1.76483938420678,
7.19114243965136));
#17207=CARTESIAN_POINT('Ctrl Pts',(-0.456628689115353,-1.75197132856033,
7.18851663724823));
#17208=CARTESIAN_POINT('Ctrl Pts',(-0.522247153731527,-1.73553989954365,
7.18589042924469));
#17209=CARTESIAN_POINT('Ctrl Pts',(-0.542667798244601,-1.73042639417967,
7.18507314617701));
#17210=CARTESIAN_POINT('Ctrl Pts',(-0.563010584939934,-1.72496745463069,
7.1842558238281));
#17211=CARTESIAN_POINT('Ctrl Pts',(-0.583265123016525,-1.71916221233715,
7.18343833365983));
#17212=CARTESIAN_POINT('Ctrl Pts',(-0.594324986363522,-1.71599229623144,
7.18299194828612));
#17213=CARTESIAN_POINT('Ctrl Pts',(-0.605348577565269,-1.71272196767285,
7.18254591460309));
#17214=CARTESIAN_POINT('Ctrl Pts',(-0.616333858846904,-1.70935174383982,
7.18210023125036));
#17215=CARTESIAN_POINT('Ctrl Pts',(-0.683725730938223,-1.68867628841438,
7.17936607863924));
#17216=CARTESIAN_POINT('Ctrl Pts',(-0.749681756569652,-1.66424383897131,
7.17664487770965));
#17217=CARTESIAN_POINT('Ctrl Pts',(-0.813838416597903,-1.63611281928401,
7.17393200937892));
#17218=CARTESIAN_POINT('Ctrl Pts',(-0.876849560193779,-1.60848407863208,
7.17126757928126));
#17219=CARTESIAN_POINT('Ctrl Pts',(-0.938126029319885,-1.57728744952324,
7.16861118688198));
#17220=CARTESIAN_POINT('Ctrl Pts',(-0.997312296090875,-1.54253001527406,
7.16595845612799));
#17221=CARTESIAN_POINT('Ctrl Pts',(-1.02347117496609,-1.52716808146505,
7.16478601417029));
#17222=CARTESIAN_POINT('Ctrl Pts',(-1.0492215115725,-1.51110995120918,7.16361428748691));
#17223=CARTESIAN_POINT('Ctrl Pts',(-1.07453112510484,-1.49435330423123,
7.16244289826465));
#17224=CARTESIAN_POINT('Ctrl Pts',(-1.10516814559263,-1.47406955963299,
7.16102494395429));
#17225=CARTESIAN_POINT('Ctrl Pts',(-1.13515946112038,-1.45276234916859,
7.15960748412057));
#17226=CARTESIAN_POINT('Ctrl Pts',(-1.16448435570839,-1.43047866030764,
7.15818984863178));
#17227=CARTESIAN_POINT('Ctrl Pts',(-1.17968931872586,-1.41892456370188,
7.15745480438074));
#17228=CARTESIAN_POINT('Ctrl Pts',(-1.1947150759586,-1.40710789339051,7.15671971290617));
#17229=CARTESIAN_POINT('Ctrl Pts',(-1.20955844125675,-1.39503487170675,
7.15598448079515));
#17230=CARTESIAN_POINT('Ctrl Pts',(-1.2184705964626,-1.38778606788849,7.1555430375945));
#17231=CARTESIAN_POINT('Ctrl Pts',(-1.22730979594949,-1.38045068721632,
7.15510189992037));
#17232=CARTESIAN_POINT('Ctrl Pts',(-1.23607420347025,-1.37303174210186,
7.15466112096385));
#17233=CARTESIAN_POINT('Ctrl Pts',(-1.28876418024182,-1.32843043336258,
7.1520112404185));
#17234=CARTESIAN_POINT('Ctrl Pts',(-1.33877042848354,-1.2807988909053,7.14937346465996));
#17235=CARTESIAN_POINT('Ctrl Pts',(-1.38599825103533,-1.23050256527184,
7.14674359103655));
#17236=CARTESIAN_POINT('Ctrl Pts',(-1.43425343070737,-1.17911213270163,
7.14405650919887));
#17237=CARTESIAN_POINT('Ctrl Pts',(-1.47960859192691,-1.1249390060584,7.14137767702936));
#17238=CARTESIAN_POINT('Ctrl Pts',(-1.52193138288134,-1.06832685423381,
7.13870261160338));
#17239=CARTESIAN_POINT('Ctrl Pts',(-1.55066539724144,-1.02989143098312,
7.13688644195504));
#17240=CARTESIAN_POINT('Ctrl Pts',(-1.57800101601077,-0.990330805152557,
7.13507200854792));
#17241=CARTESIAN_POINT('Ctrl Pts',(-1.60388667803358,-0.949743456777433,
7.13325790847962));
#17242=CARTESIAN_POINT('Ctrl Pts',(-1.62003594041973,-0.924422267854757,
7.13212614766269));
#17243=CARTESIAN_POINT('Ctrl Pts',(-1.63562069179463,-0.898701332888775,
7.13099451658541));
#17244=CARTESIAN_POINT('Ctrl Pts',(-1.65062655993749,-0.872603512387977,
7.12986267459833));
#17245=CARTESIAN_POINT('Ctrl Pts',(-1.65635574489922,-0.862639461036616,
7.12943054151348));
#17246=CARTESIAN_POINT('Ctrl Pts',(-1.66200053139848,-0.852620464599865,
7.12899837768465));
#17247=CARTESIAN_POINT('Ctrl Pts',(-1.66756006049801,-0.842547771324513,
7.12856616415337));
#17248=CARTESIAN_POINT('Ctrl Pts',(-1.67344140782474,-0.831892011347815,
7.12810893156204));
#17249=CARTESIAN_POINT('Ctrl Pts',(-1.67922337730384,-0.821183277061747,
7.1276519494335));
#17250=CARTESIAN_POINT('Ctrl Pts',(-1.68490302697532,-0.810427767612281,
7.1271953846437));
#17251=CARTESIAN_POINT('Ctrl Pts',(-1.71867201689079,-0.746479687863883,
7.12448082781816));
#17252=CARTESIAN_POINT('Ctrl Pts',(-1.74885449180758,-0.680831600304512,
7.12177889893296));
#17253=CARTESIAN_POINT('Ctrl Pts',(-1.77532011389704,-0.613841133314895,
7.11908508207449));
#17254=CARTESIAN_POINT('Ctrl Pts',(-1.80172135822353,-0.547013620983615,
7.11639781793949));
#17255=CARTESIAN_POINT('Ctrl Pts',(-1.82442431805884,-0.478849290745972,
7.11371862641413));
#17256=CARTESIAN_POINT('Ctrl Pts',(-1.84325651205081,-0.409674689769748,
7.11104302445964));
#17257=CARTESIAN_POINT('Ctrl Pts',(-1.86148527154818,-0.34271663033918,
7.10845315603751));
#17258=CARTESIAN_POINT('Ctrl Pts',(-1.87608759212419,-0.274811091848995,
7.10586665083265));
#17259=CARTESIAN_POINT('Ctrl Pts',(-1.88686151657838,-0.206241373327113,
7.1032794430912));
#17260=CARTESIAN_POINT('Ctrl Pts',(-1.8894237591873,-0.189934199908044,
7.10266415625292));
#17261=CARTESIAN_POINT('Ctrl Pts',(-1.89176925852511,-0.173589436851263,
7.10204882968071));
#17262=CARTESIAN_POINT('Ctrl Pts',(-1.89389487850133,-0.157210868172391,
7.10143340868806));
#17263=CARTESIAN_POINT('Ctrl Pts',(-1.89540717923759,-0.145558116622667,
7.10099555919912));
#17264=CARTESIAN_POINT('Ctrl Pts',(-1.89680805540638,-0.133888495556873,
7.10055767143479));
#17265=CARTESIAN_POINT('Ctrl Pts',(-1.89809506960791,-0.12221735851089,
7.10012024866215));
#17266=CARTESIAN_POINT('Ctrl Pts',(-1.90260558085945,-0.0813143172688235,
7.09858724278285));
#17267=CARTESIAN_POINT('Ctrl Pts',(-1.90572389008592,-0.0403491830271802,
7.09705830708501));
#17268=CARTESIAN_POINT('Ctrl Pts',(-1.90742224034152,0.000616434489977578,
7.09553262952215));
#17269=CARTESIAN_POINT('',(0.084982434829279,1.94905960819019,7.046));
#17270=CARTESIAN_POINT('Ctrl Pts',(0.0849160311153282,1.94854955259671,
7.046));
#17271=CARTESIAN_POINT('Ctrl Pts',(0.0133469932817959,1.94202022424704,
7.05556311378236));
#17272=CARTESIAN_POINT('Ctrl Pts',(-0.057643443386169,1.9317481562341,7.06516697216295));
#17273=CARTESIAN_POINT('Ctrl Pts',(-0.127716536696194,1.91775362299336,
7.07483035053949));
#17274=CARTESIAN_POINT('Ctrl Pts',(-0.195999508457667,1.90411660095032,
7.08424686352096));
#17275=CARTESIAN_POINT('Ctrl Pts',(-0.263412231749455,1.88694439734026,
7.09371989428859));
#17276=CARTESIAN_POINT('Ctrl Pts',(-0.329616946053496,1.86621372408347,
7.10326681575032));
#17277=CARTESIAN_POINT('Ctrl Pts',(-0.373950818831073,1.85233146448275,
7.10965989524551));
#17278=CARTESIAN_POINT('Ctrl Pts',(-0.41774246810674,1.83685263442241,7.11608610945697));
#17279=CARTESIAN_POINT('Ctrl Pts',(-0.460881457798893,1.81976080684648,
7.12255067528795));
#17280=CARTESIAN_POINT('Ctrl Pts',(-0.497884301533585,1.80510014303758,
7.12809571287374));
#17281=CARTESIAN_POINT('Ctrl Pts',(-0.53440686918178,1.7892525808674,7.13366896766314));
#17282=CARTESIAN_POINT('Ctrl Pts',(-0.570374125039445,1.77220369526276,
7.13927373202269));
#17283=CARTESIAN_POINT('Ctrl Pts',(-0.580625413497348,1.76734446872319,
7.14087118656344));
#17284=CARTESIAN_POINT('Ctrl Pts',(-0.590829427779041,1.7623885644236,7.14247087519816));
#17285=CARTESIAN_POINT('Ctrl Pts',(-0.600974912742468,1.75734066833771,
7.14407135449713));
#17286=CARTESIAN_POINT('Ctrl Pts',(-0.660532286239387,1.72770783820246,
7.15346670067592));
#17287=CARTESIAN_POINT('Ctrl Pts',(-0.718171394717493,1.69486290257124,
7.16290421661148));
#17288=CARTESIAN_POINT('Ctrl Pts',(-0.77359140837187,1.65879255638639,7.17240215454285));
#17289=CARTESIAN_POINT('Ctrl Pts',(-0.79145555504589,1.64716560228914,7.17546373004814));
#17290=CARTESIAN_POINT('Ctrl Pts',(-0.809088855973432,1.63520322368412,
7.17853158362642));
#17291=CARTESIAN_POINT('Ctrl Pts',(-0.826480388876073,1.62290416848565,
7.18160632658995));
#17292=CARTESIAN_POINT('Ctrl Pts',(-0.88415727734301,1.5821158585131,7.19180333498275));
#17293=CARTESIAN_POINT('Ctrl Pts',(-0.93917932864386,1.5376265413157,7.20207611531283));
#17294=CARTESIAN_POINT('Ctrl Pts',(-0.99133911172057,1.48977648468554,7.21244696501856));
#17295=CARTESIAN_POINT('Ctrl Pts',(-1.03697892191269,1.44790768513415,7.22152145851107));
#17296=CARTESIAN_POINT('Ctrl Pts',(-1.0804266997828,1.40346470822021,7.2306710363693));
#17297=CARTESIAN_POINT('Ctrl Pts',(-1.12150612234599,1.35666626833897,7.23991063613496));
#17298=CARTESIAN_POINT('Ctrl Pts',(-1.12930267296081,1.34778429331443,7.24166423934404));
#17299=CARTESIAN_POINT('Ctrl Pts',(-1.13701438607344,1.338816634524,7.24342123717376));
#17300=CARTESIAN_POINT('Ctrl Pts',(-1.14462934985433,1.32977774514085,7.24517924126443));
#17301=CARTESIAN_POINT('Ctrl Pts',(-1.18689780114357,1.27960549657953,7.25493741115345));
#17302=CARTESIAN_POINT('Ctrl Pts',(-1.22626964349749,1.22715044372182,7.26474446593405));
#17303=CARTESIAN_POINT('Ctrl Pts',(-1.2626041554744,1.17270468062558,7.27462138727731));
#17304=CARTESIAN_POINT('Ctrl Pts',(-1.29870272792618,1.11861246314731,7.28443417245898));
#17305=CARTESIAN_POINT('Ctrl Pts',(-1.33180351900955,1.06255418531111,7.29431591978697));
#17306=CARTESIAN_POINT('Ctrl Pts',(-1.36171904589852,1.00480435475497,7.30428720484495));
#17307=CARTESIAN_POINT('Ctrl Pts',(-1.39100085763464,0.948277866941019,
7.31404726332289));
#17308=CARTESIAN_POINT('Ctrl Pts',(-1.41723097430462,0.890129769006774,
7.32389310626744));
#17309=CARTESIAN_POINT('Ctrl Pts',(-1.44018415693848,0.83062133555421,7.33384402917814));
#17310=CARTESIAN_POINT('Ctrl Pts',(-1.44632047771148,0.814712307068312,
7.33650431624776));
#17311=CARTESIAN_POINT('Ctrl Pts',(-1.45222231211246,0.798706119319694,
7.33917211349499));
#17312=CARTESIAN_POINT('Ctrl Pts',(-1.45788473508532,0.78260794455952,7.34184778960142));
#17313=CARTESIAN_POINT('Ctrl Pts',(-1.46140114941093,0.772610836852428,
7.34350940792919));
#17314=CARTESIAN_POINT('Ctrl Pts',(-1.4648248277114,0.762579164108622,7.34517391187186));
#17315=CARTESIAN_POINT('Ctrl Pts',(-1.46815093425694,0.752525994362274,
7.34683944075502));
#17316=CARTESIAN_POINT('Ctrl Pts',(-1.4875809575628,0.693798674658319,7.35656891411169));
#17317=CARTESIAN_POINT('Ctrl Pts',(-1.50372373374688,0.634230525264841,
7.36635120065226));
#17318=CARTESIAN_POINT('Ctrl Pts',(-1.51642546703182,0.574066612526935,
7.37620769393241));
#17319=CARTESIAN_POINT('Ctrl Pts',(-1.52890893161854,0.514936566476241,
7.385894811592));
#17320=CARTESIAN_POINT('Ctrl Pts',(-1.53806859003218,0.455230176794947,
7.39565360754218));
#17321=CARTESIAN_POINT('Ctrl Pts',(-1.54370934814325,0.395188284726392,
7.40550439129109));
#17322=CARTESIAN_POINT('Ctrl Pts',(-1.54918565956382,0.33689681170573,7.41506799222619));
#17323=CARTESIAN_POINT('Ctrl Pts',(-1.55134510253712,0.278288450517533,
7.42471829564676));
#17324=CARTESIAN_POINT('Ctrl Pts',(-1.54996382900015,0.219602494440036,
7.43447388607445));
#17325=CARTESIAN_POINT('Ctrl Pts',(-1.54949240817649,0.199573310494113,
7.43780341375428));
#17326=CARTESIAN_POINT('Ctrl Pts',(-1.5486081708139,0.179535297751125,7.44114520545616));
#17327=CARTESIAN_POINT('Ctrl Pts',(-1.54730100999696,0.159498697368912,
7.4445));
#17328=CARTESIAN_POINT('',(-1.49051052577446,1.26051379553366,7.046));
#17329=CARTESIAN_POINT('Origin',(0.,0.,7.046));
#17330=CARTESIAN_POINT('Ctrl Pts',(-1.90742224034152,0.000616434489977578,
7.09553262952215));
#17331=CARTESIAN_POINT('Ctrl Pts',(-1.90876164805009,0.0329240599094907,
7.09432940051696));
#17332=CARTESIAN_POINT('Ctrl Pts',(-1.90921779267002,0.0652320529994964,
7.09312819770054));
#17333=CARTESIAN_POINT('Ctrl Pts',(-1.90877477964874,0.0975109530601205,
7.09192862283081));
#17334=CARTESIAN_POINT('Ctrl Pts',(-1.90781024899833,0.16778877103618,7.08931690111213));
#17335=CARTESIAN_POINT('Ctrl Pts',(-1.90258719753853,0.237928585345474,
7.08671289622934));
#17336=CARTESIAN_POINT('Ctrl Pts',(-1.89333689480301,0.307653748465392,
7.08411249814515));
#17337=CARTESIAN_POINT('Ctrl Pts',(-1.88389965579861,0.378787964046921,
7.0814595494873));
#17338=CARTESIAN_POINT('Ctrl Pts',(-1.87027048866354,0.449491484193812,
7.0788103548782));
#17339=CARTESIAN_POINT('Ctrl Pts',(-1.8526408196263,0.519466411196971,7.0761605500361));
#17340=CARTESIAN_POINT('Ctrl Pts',(-1.84839799409914,0.536306852496432,
7.07552283757523));
#17341=CARTESIAN_POINT('Ctrl Pts',(-1.8439232315986,0.553105040705889,7.07488508977019));
#17342=CARTESIAN_POINT('Ctrl Pts',(-1.83921877202327,0.569856697426902,
7.07424724578707));
#17343=CARTESIAN_POINT('Ctrl Pts',(-1.83514299244073,0.584369748149054,
7.07369464002192));
#17344=CARTESIAN_POINT('Ctrl Pts',(-1.83089368872409,0.598851100707912,
7.07314183740804));
#17345=CARTESIAN_POINT('Ctrl Pts',(-1.82648012174354,0.613273349358239,
7.07258974257699));
#17346=CARTESIAN_POINT('Ctrl Pts',(-1.80525925753629,0.682616939592868,
7.06993521631944));
#17347=CARTESIAN_POINT('Ctrl Pts',(-1.78021580797096,0.750706522102631,
7.06729279368472));
#17348=CARTESIAN_POINT('Ctrl Pts',(-1.75159954554489,0.817253861437449,
7.06465826007958));
#17349=CARTESIAN_POINT('Ctrl Pts',(-1.72257788914062,0.884743947600279,
7.06198640419794));
#17350=CARTESIAN_POINT('Ctrl Pts',(-1.68988110151814,0.950648721336099,
7.05932266244995));
#17351=CARTESIAN_POINT('Ctrl Pts',(-1.65371662519363,1.01465825897231,7.05666263857406));
#17352=CARTESIAN_POINT('Ctrl Pts',(-1.61767133058481,1.07845685019671,7.05401138093072));
#17353=CARTESIAN_POINT('Ctrl Pts',(-1.57818065931587,1.14037360389397,7.051363816695));
#17354=CARTESIAN_POINT('Ctrl Pts',(-1.53540446982221,1.20007853919048,7.04871559292653));
#17355=CARTESIAN_POINT('Ctrl Pts',(-1.52078518671176,1.2204834271088,7.04781053023934));
#17356=CARTESIAN_POINT('Ctrl Pts',(-1.50578179227618,1.24062970905854,7.04690539051781));
#17357=CARTESIAN_POINT('Ctrl Pts',(-1.49039960333531,1.26050328917698,7.046));
#17358=CARTESIAN_POINT('',(-1.,-1.22464679914735E-16,8.));
#17359=CARTESIAN_POINT('',(-1.5,-1.83697019872103E-16,7.5));
#17360=CARTESIAN_POINT('Origin',(0.,0.,8.));
#17361=CARTESIAN_POINT('Ctrl Pts',(1.13509973994373,-1.59049193030951,-0.230074082272067));
#17362=CARTESIAN_POINT('Ctrl Pts',(1.66385265555159,-1.21313239420412,-0.193036768839232));
#17363=CARTESIAN_POINT('Ctrl Pts',(2.30633309595034,0.10379526882931,-0.11896214197356));
#17364=CARTESIAN_POINT('Ctrl Pts',(1.1618831159781,1.99754257541113,-0.00785020167505245));
#17365=CARTESIAN_POINT('Ctrl Pts',(-1.04657265959996,2.05782619857144,0.103261738623455));
#17366=CARTESIAN_POINT('Ctrl Pts',(-2.29698513032901,0.238308494988224,
0.214373678921962));
#17367=CARTESIAN_POINT('Ctrl Pts',(-1.44610949780919,-1.80077244555215,
0.32548561922047));
#17368=CARTESIAN_POINT('Ctrl Pts',(0.727982080133343,-2.19148935509534,
0.436597559518978));
#17369=CARTESIAN_POINT('Ctrl Pts',(2.23595404085407,-0.577589325353924,
0.547709499817485));
#17370=CARTESIAN_POINT('Ctrl Pts',(1.69824597043106,1.56497940407905,0.658821440115993));
#17371=CARTESIAN_POINT('Ctrl Pts',(-0.393241729595879,2.27560136836119,
0.7699333804145));
#17372=CARTESIAN_POINT('Ctrl Pts',(-2.12493397204,0.90429099396703,0.881045320713008));
#17373=CARTESIAN_POINT('Ctrl Pts',(-1.91248731439823,-1.29440519809075,
0.992157261011514));
#17374=CARTESIAN_POINT('Ctrl Pts',(0.0497351526023427,-2.30880745912378,
1.10326920131002));
#17375=CARTESIAN_POINT('Ctrl Pts',(1.96645238083605,-1.21084445058012,1.21438114160853));
#17376=CARTESIAN_POINT('Ctrl Pts',(2.0840238587571,0.994948952062592,1.32549308190704));
#17377=CARTESIAN_POINT('Ctrl Pts',(0.294879848465431,2.29044125875909,1.43660502220554));
#17378=CARTESIAN_POINT('Ctrl Pts',(-1.76405540105404,1.49036437523231,1.54771696250405));
#17379=CARTESIAN_POINT('Ctrl Pts',(-2.20902124244616,-0.673277315499274,
1.65882890280256));
#17380=CARTESIAN_POINT('Ctrl Pts',(-0.63290935858251,-2.22092378987733,
1.76994084310107));
#17381=CARTESIAN_POINT('Ctrl Pts',(1.5222639082646,-1.73660290660664,1.88105278339957));
#17382=CARTESIAN_POINT('Ctrl Pts',(2.28468753295219,0.336570763856544,1.99216472369808));
#17383=CARTESIAN_POINT('Ctrl Pts',(0.956804884638204,2.10180906822536,2.10327666399659));
#17384=CARTESIAN_POINT('Ctrl Pts',(-1.24647766157407,1.94406029583798,2.2143886042951));
#17385=CARTESIAN_POINT('Ctrl Pts',(-2.30933289737607,0.00765190922063762,
2.3255005445936));
#17386=CARTESIAN_POINT('Ctrl Pts',(-1.25933333160116,-1.9357573546638,2.43661248489211));
#17387=CARTESIAN_POINT('Ctrl Pts',(0.942855455692524,-2.10810354889204,
2.54772442519062));
#17388=CARTESIAN_POINT('Ctrl Pts',(2.28240695194457,-0.35170369161106,2.65883636548913));
#17389=CARTESIAN_POINT('Ctrl Pts',(1.53373873309094,1.72647689788489,2.76994830578763));
#17390=CARTESIAN_POINT('Ctrl Pts',(-0.618177691355928,2.22506928503553,
2.88106024608615));
#17391=CARTESIAN_POINT('Ctrl Pts',(-2.20451099698397,0.687901333838673,
2.99217218638465));
#17392=CARTESIAN_POINT('Ctrl Pts',(-1.77389315295183,-1.47864128941955,
3.10328412668316));
#17393=CARTESIAN_POINT('Ctrl Pts',(0.279694972942425,-2.29234545893725,
3.21439606698166));
#17394=CARTESIAN_POINT('Ctrl Pts',(2.07738458076118,-1.00873697491097,3.32550800728017));
#17395=CARTESIAN_POINT('Ctrl Pts',(1.97443353669272,1.1977851185115,3.43661994757868));
#17396=CARTESIAN_POINT('Ctrl Pts',(0.0650338075591902,2.30842967941821,
3.54773188787719));
#17397=CARTESIAN_POINT('Ctrl Pts',(-1.90386665125239,1.30704581219857,3.65884382817569));
#17398=CARTESIAN_POINT('Ctrl Pts',(-2.13088147818969,-0.890180378860142,
3.7699557684742));
#17399=CARTESIAN_POINT('Ctrl Pts',(-0.408310273068383,-2.2729627585538,
3.88106770877271));
#17400=CARTESIAN_POINT('Ctrl Pts',(1.6878321574451,-1.57616610457607,3.99217964907122));
#17401=CARTESIAN_POINT('Ctrl Pts',(2.23974323019256,0.562696404915903,4.10329158936972));
#17402=CARTESIAN_POINT('Ctrl Pts',(0.742468479097436,2.18673673263618,4.21440352966824));
#17403=CARTESIAN_POINT('Ctrl Pts',(-1.43410551503643,1.81008794060395,4.32551546996673));
#17404=CARTESIAN_POINT('Ctrl Pts',(-2.29858772583325,-0.222646468261011,
4.43662741026525));
#17405=CARTESIAN_POINT('Ctrl Pts',(-1.06004610686433,-2.05167717429874,
4.54773935056375));
#17406=CARTESIAN_POINT('Ctrl Pts',(1.14835286831205,-2.00358745066383,4.65885129086226));
#17407=CARTESIAN_POINT('Ctrl Pts',(2.30610086989477,-0.122375538925838,
4.76996323116077));
#17408=CARTESIAN_POINT('Ctrl Pts',(1.35395110677505,1.87080018895779,4.88107517145928));
#17409=CARTESIAN_POINT('Ctrl Pts',(-0.836955550366062,2.15234346911026,
4.99218711175778));
#17410=CARTESIAN_POINT('Ctrl Pts',(-2.26211489466594,0.464664680140549,
5.10329905205629));
#17411=CARTESIAN_POINT('Ctrl Pts',(-1.61762005706343,-1.64814504446985,
5.2144109923548));
#17412=CARTESIAN_POINT('Ctrl Pts',(0.506867541264277,-2.25303406293758,
5.3255229326533));
#17413=CARTESIAN_POINT('Ctrl Pts',(2.16761217480869,-0.796576982199858,
5.43663487295182));
#17414=CARTESIAN_POINT('Ctrl Pts',(1.84516460593919,1.38868385957575,5.54774681325032));
#17415=CARTESIAN_POINT('Ctrl Pts',(-0.165459925935554,2.30341092165264,
5.65885875354883));
#17416=CARTESIAN_POINT('Ctrl Pts',(-2.02470376163623,1.11069974665188,5.76997069384733));
#17417=CARTESIAN_POINT('Ctrl Pts',(-2.03150206860296,-1.09820982237999,
5.88108263414585));
#17418=CARTESIAN_POINT('Ctrl Pts',(-0.179645428808579,-2.30235098638037,
5.99219457444435));
#17419=CARTESIAN_POINT('Ctrl Pts',(1.83658550522895,-1.40001438181273,6.10330651474285));
#17420=CARTESIAN_POINT('Ctrl Pts',(2.17246271157681,0.783202663677277,6.21441845504137));
#17421=CARTESIAN_POINT('Ctrl Pts',(0.520757933621259,2.24989134978725,6.32553039533987));
#17422=CARTESIAN_POINT('Ctrl Pts',(-1.60748926038381,1.65803443249082,6.43664233563838));
#17423=CARTESIAN_POINT('Ctrl Pts',(-2.26483986170582,-0.450648314453544,
6.54775427593688));
#17424=CARTESIAN_POINT('Ctrl Pts',(-0.850371985170964,-2.14729633892256,
6.6588662162354));
#17425=CARTESIAN_POINT('Ctrl Pts',(1.34274482878903,-1.87882089420371,6.7699781565339));
#17426=CARTESIAN_POINT('Ctrl Pts',(2.30616083080651,0.107634649639171,6.88109009683241));
#17427=CARTESIAN_POINT('Ctrl Pts',(1.16193045799902,1.99751503787814,6.99220203713092));
#17428=CARTESIAN_POINT('Ctrl Pts',(-1.04999517826429,2.05607780322851,7.10331397742942));
#17429=CARTESIAN_POINT('Ctrl Pts',(-1.87709151778098,0.84653605896511,7.1773886042951));
#17430=CARTESIAN_POINT('Ctrl Pts',(-1.94370052943366,0.200360305148756,
7.21442591772793));
#17431=CARTESIAN_POINT('Ctrl Pts',(1.05793541951256,-1.48236995244729,-0.153382721514712));
#17432=CARTESIAN_POINT('Ctrl Pts',(1.55074360006928,-1.13066339742992,-0.116345408081876));
#17433=CARTESIAN_POINT('Ctrl Pts',(2.14954808422461,0.0967392444982914,
-0.0422707812162042));
#17434=CARTESIAN_POINT('Ctrl Pts',(1.08289805597856,1.8617492085907,0.0688411590823027));
#17435=CARTESIAN_POINT('Ctrl Pts',(-0.975426428816855,1.91793473829667,
0.179953099380811));
#17436=CARTESIAN_POINT('Ctrl Pts',(-2.14083559528361,0.222108233089066,
0.291065039679317));
#17437=CARTESIAN_POINT('Ctrl Pts',(-1.34780266824982,-1.6783555537827,0.402176979977826));
#17438=CARTESIAN_POINT('Ctrl Pts',(0.678493704334455,-2.04251144516605,
0.513288920276332));
#17439=CARTESIAN_POINT('Ctrl Pts',(2.08395341218121,-0.538324680837788,
0.624400860574841));
#17440=CARTESIAN_POINT('Ctrl Pts',(1.58279885012795,1.4585917731467,0.735512800873347));
#17441=CARTESIAN_POINT('Ctrl Pts',(-0.366509073634787,2.12090550597771,
0.846624741171857));
#17442=CARTESIAN_POINT('Ctrl Pts',(-1.9804805111294,0.842817100910752,0.957736681470361));
#17443=CARTESIAN_POINT('Ctrl Pts',(-1.78247602221336,-1.20641125891655,
1.06884862176887));
#17444=CARTESIAN_POINT('Ctrl Pts',(0.0463541464078725,-2.15185423966612,
1.17996056206738));
#17445=CARTESIAN_POINT('Ctrl Pts',(1.83277253201941,-1.12853098869745,1.29107250236589));
#17446=CARTESIAN_POINT('Ctrl Pts',(1.94235147600127,0.927312111837943,1.40218444266439));
#17447=CARTESIAN_POINT('Ctrl Pts',(0.274833853990247,2.13473657748725,1.5132963829629));
#17448=CARTESIAN_POINT('Ctrl Pts',(-1.6441345417364,1.38904908974441,1.62440832326141));
#17449=CARTESIAN_POINT('Ctrl Pts',(-2.05885151110621,-0.627507781172011,
1.73552026355991));
#17450=CARTESIAN_POINT('Ctrl Pts',(-0.589884046505544,-2.06994492084524,
1.84663220385842));
#17451=CARTESIAN_POINT('Ctrl Pts',(1.4187800857734,-1.6185482736686,1.95774414415693));
#17452=CARTESIAN_POINT('Ctrl Pts',(2.12937399117781,0.313690612134129,2.06885608445544));
#17453=CARTESIAN_POINT('Ctrl Pts',(0.891761086185737,1.95892764316774,2.17996802475395));
#17454=CARTESIAN_POINT('Ctrl Pts',(-1.16174184647048,1.81190266569614,2.29107996505245));
#17455=CARTESIAN_POINT('Ctrl Pts',(-2.15234395851487,0.00713173081318942,
2.40219190535096));
#17456=CARTESIAN_POINT('Ctrl Pts',(-1.17372358532974,-1.80416416021932,
2.51330384564946));
#17457=CARTESIAN_POINT('Ctrl Pts',(0.878759942370547,-1.96479422370721,
2.62441578594798));
#17458=CARTESIAN_POINT('Ctrl Pts',(2.1272484445495,-0.327794800258781,2.73552772624649));
#17459=CARTESIAN_POINT('Ctrl Pts',(1.42947484958074,1.60911063316174,2.84663966654499));
#17460=CARTESIAN_POINT('Ctrl Pts',(-0.576153841133258,2.07380860436568,
2.9577516068435));
#17461=CARTESIAN_POINT('Ctrl Pts',(-2.0546478730846,0.641137655651238,3.068863547142));
#17462=CARTESIAN_POINT('Ctrl Pts',(-1.65330352117917,-1.37812294178502,
3.17997548744051));
#17463=CARTESIAN_POINT('Ctrl Pts',(0.260681249517398,-2.1365113297345,3.29108742773902));
#17464=CARTESIAN_POINT('Ctrl Pts',(1.93616353752793,-0.940162821976462,
3.40219936803753));
#17465=CARTESIAN_POINT('Ctrl Pts',(1.84021112721267,1.11635943278533,3.51331130833604));
#17466=CARTESIAN_POINT('Ctrl Pts',(0.0606127955645832,2.15150214150485,
3.62442324863454));
#17467=CARTESIAN_POINT('Ctrl Pts',(-1.77444139357172,1.21819256140342,3.73553518893305));
#17468=CARTESIAN_POINT('Ctrl Pts',(-1.98602370455295,-0.829665728403687,
3.84664712923155));
#17469=CARTESIAN_POINT('Ctrl Pts',(-0.380553254334539,-2.11844626942319,
3.95775906953007));
#17470=CARTESIAN_POINT('Ctrl Pts',(1.57309297035165,-1.46901799937757,4.06887100982856));
#17471=CARTESIAN_POINT('Ctrl Pts',(2.08748501162692,0.524444184281487,4.17998295012709));
#17472=CARTESIAN_POINT('Ctrl Pts',(0.691995314832617,2.038081906987,4.29109489042558));
#17473=CARTESIAN_POINT('Ctrl Pts',(-1.33661471876519,1.68703777951035,4.4022068307241));
#17474=CARTESIAN_POINT('Ctrl Pts',(-2.14232924600648,-0.207510914251802,
4.5133187710226));
#17475=CARTESIAN_POINT('Ctrl Pts',(-0.987983948286119,-1.91220372599474,
4.62443071132112));
#17476=CARTESIAN_POINT('Ctrl Pts',(1.07028759741094,-1.86738315194504,4.73554265161961));
#17477=CARTESIAN_POINT('Ctrl Pts',(2.14933164494543,-0.114056423903322,
4.84665459191812));
#17478=CARTESIAN_POINT('Ctrl Pts',(1.26190922413262,1.74362279637852,4.95776653221663));
#17479=CARTESIAN_POINT('Ctrl Pts',(-0.780059135009386,2.00602670479084,
5.06887847251514));
#17480=CARTESIAN_POINT('Ctrl Pts',(-2.10833584561709,0.433076676893185,
5.17999041281365));
#17481=CARTESIAN_POINT('Ctrl Pts',(-1.50765390340601,-1.53610379571154,
5.29110235311216));
#17482=CARTESIAN_POINT('Ctrl Pts',(0.472410578590484,-2.0998723307505,5.40221429341067));
#17483=CARTESIAN_POINT('Ctrl Pts',(2.02025744064608,-0.742425510448462,
5.51332623370916));
#17484=CARTESIAN_POINT('Ctrl Pts',(1.71972992571626,1.29428083705086,5.62443817400769));
#17485=CARTESIAN_POINT('Ctrl Pts',(-0.154211925170411,2.14682455995381,
5.73555011430617));
#17486=CARTESIAN_POINT('Ctrl Pts',(-1.88706397163077,1.03519414292605,5.8466620546047));
#17487=CARTESIAN_POINT('Ctrl Pts',(-1.89340012825184,-1.02355328634819,
5.95777399490319));
#17488=CARTESIAN_POINT('Ctrl Pts',(-0.167433094557426,-2.14583667930556,
6.0688859352017));
#17489=CARTESIAN_POINT('Ctrl Pts',(1.71173403408707,-1.3048411079894,6.17999787550022));
#17490=CARTESIAN_POINT('Ctrl Pts',(2.02477823689865,0.729960380928156,6.29110981579872));
#17491=CARTESIAN_POINT('Ctrl Pts',(0.485356699136765,2.09694325990492,6.40222175609723));
#17492=CARTESIAN_POINT('Ctrl Pts',(-1.49821180042767,1.54532090104292,6.51333369639574));
#17493=CARTESIAN_POINT('Ctrl Pts',(-2.11087556882117,-0.420013146710507,
6.62444563669424));
#17494=CARTESIAN_POINT('Ctrl Pts',(-0.792563517738235,-2.00132267958093,
6.73555757699275));
#17495=CARTESIAN_POINT('Ctrl Pts',(1.2514647512946,-1.75109825238519,6.84666951729126));
#17496=CARTESIAN_POINT('Ctrl Pts',(2.1493875297017,0.100317623388547,6.95778145758976));
#17497=CARTESIAN_POINT('Ctrl Pts',(1.08294217967889,1.86172354306503,7.06889339788828));
#17498=CARTESIAN_POINT('Ctrl Pts',(-0.978616283938414,1.91630519923899,
7.18000533818678));
#17499=CARTESIAN_POINT('Ctrl Pts',(-1.74948643933749,0.788988358607273,
7.25407996505245));
#17500=CARTESIAN_POINT('Ctrl Pts',(-1.8115673562881,0.186739769222141,7.29111727848529));
#17501=CARTESIAN_POINT('Ctrl Pts',(0.980771099081382,-1.37424797458506,
-0.0766913607573567));
#17502=CARTESIAN_POINT('Ctrl Pts',(1.43763454458697,-1.04819440065571,-0.0396540473245209));
#17503=CARTESIAN_POINT('Ctrl Pts',(1.99276307249889,0.0896832201672716,
0.034420579541151));
#17504=CARTESIAN_POINT('Ctrl Pts',(1.00391299597902,1.72595584177028,0.145532519839658));
#17505=CARTESIAN_POINT('Ctrl Pts',(-0.904280198033752,1.77804327802189,
0.256644460138166));
#17506=CARTESIAN_POINT('Ctrl Pts',(-1.98468606023822,0.205907971189911,
0.367756400436673));
#17507=CARTESIAN_POINT('Ctrl Pts',(-1.24949583869046,-1.55593866201325,
0.478868340735181));
#17508=CARTESIAN_POINT('Ctrl Pts',(0.629005328535562,-1.89353353523676,
0.589980281033688));
#17509=CARTESIAN_POINT('Ctrl Pts',(1.93195278350834,-0.499060036321655,
0.701092221332196));
#17510=CARTESIAN_POINT('Ctrl Pts',(1.46735172982485,1.35220414221434,0.812204161630702));
#17511=CARTESIAN_POINT('Ctrl Pts',(-0.339776417673698,1.96620964359423,
0.923316101929211));
#17512=CARTESIAN_POINT('Ctrl Pts',(-1.8360270502188,0.781343207854476,1.03442804222772));
#17513=CARTESIAN_POINT('Ctrl Pts',(-1.65246473002849,-1.11841731974236,
1.14553998252623));
#17514=CARTESIAN_POINT('Ctrl Pts',(0.0429731402134002,-1.99490102020845,
1.25665192282473));
#17515=CARTESIAN_POINT('Ctrl Pts',(1.69909268320277,-1.04621752681478,1.36776386312324));
#17516=CARTESIAN_POINT('Ctrl Pts',(1.80067909324543,0.859675271613291,1.47887580342175));
#17517=CARTESIAN_POINT('Ctrl Pts',(0.254787859515066,1.97903189621542,1.58998774372026));
#17518=CARTESIAN_POINT('Ctrl Pts',(-1.52421368241876,1.2877338042565,1.70109968401876));
#17519=CARTESIAN_POINT('Ctrl Pts',(-1.90868177976625,-0.581738246844747,
1.81221162431727));
#17520=CARTESIAN_POINT('Ctrl Pts',(-0.54685873442858,-1.91896605181315,
1.92332356461578));
#17521=CARTESIAN_POINT('Ctrl Pts',(1.3152962632822,-1.50049364073057,2.03443550491428));
#17522=CARTESIAN_POINT('Ctrl Pts',(1.97406044940342,0.290810460411716,2.14554744521279));
#17523=CARTESIAN_POINT('Ctrl Pts',(0.826717287733271,1.81604621811011,2.2566593855113));
#17524=CARTESIAN_POINT('Ctrl Pts',(-1.0770060313669,1.6797450355543,2.36777132580981));
#17525=CARTESIAN_POINT('Ctrl Pts',(-1.99535501965367,0.00661155240574004,
2.47888326610832));
#17526=CARTESIAN_POINT('Ctrl Pts',(-1.08811383905831,-1.67257096577485,
2.58999520640682));
#17527=CARTESIAN_POINT('Ctrl Pts',(0.814664429048569,-1.82148489852237,
2.70110714670533));
#17528=CARTESIAN_POINT('Ctrl Pts',(1.97208993715443,-0.303885908906504,
2.81221908700384));
#17529=CARTESIAN_POINT('Ctrl Pts',(1.32521096607054,1.49174436843859,2.92333102730234));
#17530=CARTESIAN_POINT('Ctrl Pts',(-0.534129990910586,1.92254792369583,
3.03444296760085));
#17531=CARTESIAN_POINT('Ctrl Pts',(-1.90478474918523,0.594373977463801,
3.14555490789936));
#17532=CARTESIAN_POINT('Ctrl Pts',(-1.53271388940651,-1.27760459415048,
3.25666684819786));
#17533=CARTESIAN_POINT('Ctrl Pts',(0.241667526092368,-1.98067720053176,
3.36777878849638));
#17534=CARTESIAN_POINT('Ctrl Pts',(1.79494249429468,-0.871588669041957,
3.47889072879488));
#17535=CARTESIAN_POINT('Ctrl Pts',(1.70598871773261,1.03493374705916,3.59000266909339));
#17536=CARTESIAN_POINT('Ctrl Pts',(0.0561917835699789,1.99457460359148,
3.70111460939189));
#17537=CARTESIAN_POINT('Ctrl Pts',(-1.64501613589106,1.12933931060827,3.81222654969041));
#17538=CARTESIAN_POINT('Ctrl Pts',(-1.8411659309162,-0.769151077947235,
3.92333848998891));
#17539=CARTESIAN_POINT('Ctrl Pts',(-0.352796235600697,-1.96392978029257,
4.03445043028742));
#17540=CARTESIAN_POINT('Ctrl Pts',(1.45835378325819,-1.36186989417907,4.14556237058593));
#17541=CARTESIAN_POINT('Ctrl Pts',(1.93522679306129,0.486191963647073,4.25667431088443));
#17542=CARTESIAN_POINT('Ctrl Pts',(0.641522150567798,1.88942708133782,4.36778625118295));
#17543=CARTESIAN_POINT('Ctrl Pts',(-1.23912392249396,1.56398761841675,4.47889819148144));
#17544=CARTESIAN_POINT('Ctrl Pts',(-1.9860707661797,-0.192375360242598,
4.59001013177996));
#17545=CARTESIAN_POINT('Ctrl Pts',(-0.915921789707908,-1.77273027769074,
4.70112207207846));
#17546=CARTESIAN_POINT('Ctrl Pts',(0.992222326509824,-1.73117885322625,
4.81223401237697));
#17547=CARTESIAN_POINT('Ctrl Pts',(1.99256241999608,-0.105737308880805,
4.92334595267548));
#17548=CARTESIAN_POINT('Ctrl Pts',(1.1698673414902,1.61644540379926,5.03445789297399));
#17549=CARTESIAN_POINT('Ctrl Pts',(-0.723162719652709,1.85970994047142,
5.1455698332725));
#17550=CARTESIAN_POINT('Ctrl Pts',(-1.95455679656824,0.401488673645819,
5.25668177357099));
#17551=CARTESIAN_POINT('Ctrl Pts',(-1.39768774974859,-1.42406254695323,
5.36779371386952));
#17552=CARTESIAN_POINT('Ctrl Pts',(0.437953615916691,-1.94671059856343,
5.47890565416801));
#17553=CARTESIAN_POINT('Ctrl Pts',(1.87290270648346,-0.688274038697066,
5.59001759446653));
#17554=CARTESIAN_POINT('Ctrl Pts',(1.59429524549334,1.19987781452597,5.70112953476503));
#17555=CARTESIAN_POINT('Ctrl Pts',(-0.142963924405265,1.99023819825497,
5.81224147506354));
#17556=CARTESIAN_POINT('Ctrl Pts',(-1.74942418162531,0.959688539200224,
5.92335341536204));
#17557=CARTESIAN_POINT('Ctrl Pts',(-1.75529818790071,-0.948896750316397,
6.03446535566056));
#17558=CARTESIAN_POINT('Ctrl Pts',(-0.155220760306272,-1.98932237223074,
6.14557729595905));
#17559=CARTESIAN_POINT('Ctrl Pts',(1.58688256294519,-1.20966783416606,6.25668923625758));
#17560=CARTESIAN_POINT('Ctrl Pts',(1.8770937622205,0.676718098179033,6.36780117655607));
#17561=CARTESIAN_POINT('Ctrl Pts',(0.449955464652266,1.94399517002259,6.47891311685458));
#17562=CARTESIAN_POINT('Ctrl Pts',(-1.38893434047152,1.43260736959501,6.59002505715309));
#17563=CARTESIAN_POINT('Ctrl Pts',(-1.95691127593653,-0.389377978967469,
6.7011369974516));
#17564=CARTESIAN_POINT('Ctrl Pts',(-0.734755050305503,-1.8553490202393,
6.8122489377501));
#17565=CARTESIAN_POINT('Ctrl Pts',(1.16018467380016,-1.62337561056666,6.92336087804862));
#17566=CARTESIAN_POINT('Ctrl Pts',(1.99261422859689,0.0930005971379224,
7.03447281834711));
#17567=CARTESIAN_POINT('Ctrl Pts',(1.00395390135875,1.72593204825193,7.14558475864564));
#17568=CARTESIAN_POINT('Ctrl Pts',(-0.907237389612538,1.77653259524947,
7.25669669894413));
#17569=CARTESIAN_POINT('Ctrl Pts',(-1.62188136089401,0.731440658249439,
7.33077132580981));
#17570=CARTESIAN_POINT('Ctrl Pts',(-1.67943418314253,0.173119233295526,
7.36780863924264));
#17571=CARTESIAN_POINT('Ctrl Pts',(0.903606778650207,-1.26612599672284,
-1.38777878078145E-15));
#17572=CARTESIAN_POINT('Ctrl Pts',(1.32452548910467,-0.965725403881512,
0.0370373134328344));
#17573=CARTESIAN_POINT('Ctrl Pts',(1.83597806077316,0.082627195836251,0.111111940298506));
#17574=CARTESIAN_POINT('Ctrl Pts',(0.924927935979477,1.59016247494986,0.222223880597014));
#17575=CARTESIAN_POINT('Ctrl Pts',(-0.833133967250649,1.63815181774712,
0.333335820895521));
#17576=CARTESIAN_POINT('Ctrl Pts',(-1.82853652519283,0.189707709290757,
0.444447761194028));
#17577=CARTESIAN_POINT('Ctrl Pts',(-1.15118900913109,-1.43352177024381,
0.555559701492536));
#17578=CARTESIAN_POINT('Ctrl Pts',(0.579516952736672,-1.74455562530747,
0.666671641791043));
#17579=CARTESIAN_POINT('Ctrl Pts',(1.77995215483547,-0.45979539180552,0.777783582089551));
#17580=CARTESIAN_POINT('Ctrl Pts',(1.35190460952174,1.24581651128198,0.888895522388059));
#17581=CARTESIAN_POINT('Ctrl Pts',(-0.313043761712607,1.81151378121076,
1.00000746268657));
#17582=CARTESIAN_POINT('Ctrl Pts',(-1.6915735893082,0.719869314798195,1.11111940298507));
#17583=CARTESIAN_POINT('Ctrl Pts',(-1.52245343784362,-1.03042338056816,
1.22223134328358));
#17584=CARTESIAN_POINT('Ctrl Pts',(0.0395921340189295,-1.83794780075079,
1.33334328358209));
#17585=CARTESIAN_POINT('Ctrl Pts',(1.56541283438613,-0.96390406493211,1.44445522388059));
#17586=CARTESIAN_POINT('Ctrl Pts',(1.65900671048959,0.792038431388639,1.55556716417911));
#17587=CARTESIAN_POINT('Ctrl Pts',(0.234741865039883,1.82332721494359,1.66667910447761));
#17588=CARTESIAN_POINT('Ctrl Pts',(-1.40429282310112,1.18641851876859,1.77779104477612));
#17589=CARTESIAN_POINT('Ctrl Pts',(-1.7585120484263,-0.535968712517482,
1.88890298507462));
#17590=CARTESIAN_POINT('Ctrl Pts',(-0.503833422351614,-1.76798718278107,
2.00001492537314));
#17591=CARTESIAN_POINT('Ctrl Pts',(1.211812440791,-1.38243900779253,2.11112686567164));
#17592=CARTESIAN_POINT('Ctrl Pts',(1.81874690762903,0.2679303086893,2.22223880597015));
#17593=CARTESIAN_POINT('Ctrl Pts',(0.761673489280804,1.67316479305249,2.33335074626865));
#17594=CARTESIAN_POINT('Ctrl Pts',(-0.99227021626331,1.54758740541246,2.44446268656716));
#17595=CARTESIAN_POINT('Ctrl Pts',(-1.83836608079246,0.00609137399829168,
2.55557462686567));
#17596=CARTESIAN_POINT('Ctrl Pts',(-1.00250409278689,-1.54097777133038,
2.66668656716418));
#17597=CARTESIAN_POINT('Ctrl Pts',(0.750568915726592,-1.67817557333754,
2.77779850746269));
#17598=CARTESIAN_POINT('Ctrl Pts',(1.81693142975936,-0.279977017554228,
2.8889104477612));
#17599=CARTESIAN_POINT('Ctrl Pts',(1.22094708256035,1.37437810371544,3.0000223880597));
#17600=CARTESIAN_POINT('Ctrl Pts',(-0.492106140687917,1.77128724302598,
3.11113432835821));
#17601=CARTESIAN_POINT('Ctrl Pts',(-1.75492162528586,0.547610299276366,
3.22224626865671));
#17602=CARTESIAN_POINT('Ctrl Pts',(-1.41212425763385,-1.17708624651594,
3.33335820895523));
#17603=CARTESIAN_POINT('Ctrl Pts',(0.222653802667342,-1.82484307132901,
3.44447014925373));
#17604=CARTESIAN_POINT('Ctrl Pts',(1.65372145106143,-0.803014516107455,
3.55558208955224));
#17605=CARTESIAN_POINT('Ctrl Pts',(1.57176630825256,0.953508061332994,3.66669402985075));
#17606=CARTESIAN_POINT('Ctrl Pts',(0.0517707715753711,1.83764706567811,
3.77780597014925));
#17607=CARTESIAN_POINT('Ctrl Pts',(-1.5155908782104,1.04048605981312,3.88891791044777));
#17608=CARTESIAN_POINT('Ctrl Pts',(-1.69630815727945,-0.708636427490783,
4.00002985074626));
#17609=CARTESIAN_POINT('Ctrl Pts',(-0.325039216866852,-1.80941329116195,
4.11114179104478));
#17610=CARTESIAN_POINT('Ctrl Pts',(1.34361459616473,-1.25472178898058,4.22225373134328));
#17611=CARTESIAN_POINT('Ctrl Pts',(1.78296857449566,0.447939743012656,4.3333656716418));
#17612=CARTESIAN_POINT('Ctrl Pts',(0.591048986302979,1.74077225568864,4.44447761194029));
#17613=CARTESIAN_POINT('Ctrl Pts',(-1.14163312622272,1.44093745732314,4.55558955223881));
#17614=CARTESIAN_POINT('Ctrl Pts',(-1.82981228635293,-0.177239806233389,
4.66670149253731));
#17615=CARTESIAN_POINT('Ctrl Pts',(-0.843859631129698,-1.63325682938675,
4.77781343283583));
#17616=CARTESIAN_POINT('Ctrl Pts',(0.914157055608714,-1.59497455450745,
4.88892537313433));
#17617=CARTESIAN_POINT('Ctrl Pts',(1.83579319504673,-0.0974181938582904,
5.00003731343284));
#17618=CARTESIAN_POINT('Ctrl Pts',(1.07782545884778,1.48926801121999,5.11114925373134));
#17619=CARTESIAN_POINT('Ctrl Pts',(-0.666266304296033,1.713393176152,5.22226119402985));
#17620=CARTESIAN_POINT('Ctrl Pts',(-1.80077774751939,0.369900670398456,
5.33337313432836));
#17621=CARTESIAN_POINT('Ctrl Pts',(-1.28772159609117,-1.31202129819493,
5.44448507462686));
#17622=CARTESIAN_POINT('Ctrl Pts',(0.403496653242899,-1.79354886637635,
5.55559701492538));
#17623=CARTESIAN_POINT('Ctrl Pts',(1.72554797232085,-0.634122566945669,
5.66670895522387));
#17624=CARTESIAN_POINT('Ctrl Pts',(1.46886056527041,1.10547479200108,5.77782089552239));
#17625=CARTESIAN_POINT('Ctrl Pts',(-0.131715923640121,1.83365183655613,
5.88893283582089));
#17626=CARTESIAN_POINT('Ctrl Pts',(-1.61178439161985,0.884182935474394,
6.0000447761194));
#17627=CARTESIAN_POINT('Ctrl Pts',(-1.61719624754958,-0.874240214284601,
6.11115671641792));
#17628=CARTESIAN_POINT('Ctrl Pts',(-0.143008426055117,-1.83280806515592,
6.2222686567164));
#17629=CARTESIAN_POINT('Ctrl Pts',(1.4620310918033,-1.11449456034272,6.33338059701493));
#17630=CARTESIAN_POINT('Ctrl Pts',(1.72940928754233,0.623475815429911,6.44449253731343));
#17631=CARTESIAN_POINT('Ctrl Pts',(0.414554230167772,1.79104708014026,6.55560447761194));
#17632=CARTESIAN_POINT('Ctrl Pts',(-1.27965688051538,1.3198938381471,6.66671641791045));
#17633=CARTESIAN_POINT('Ctrl Pts',(-1.80294698305189,-0.358742811224428,
6.77782835820896));
#17634=CARTESIAN_POINT('Ctrl Pts',(-0.676946582872774,-1.70937536089767,
6.88894029850746));
#17635=CARTESIAN_POINT('Ctrl Pts',(1.06890459630572,-1.49565296874813,7.00005223880597));
#17636=CARTESIAN_POINT('Ctrl Pts',(1.83584092749207,0.0856835708872964,
7.11116417910447));
#17637=CARTESIAN_POINT('Ctrl Pts',(0.924965623038614,1.59014055343882,7.22227611940298));
#17638=CARTESIAN_POINT('Ctrl Pts',(-0.835858495286665,1.63675999125994,
7.33338805970149));
#17639=CARTESIAN_POINT('Ctrl Pts',(-1.49427628245053,0.673892957891604,
7.40746268656716));
#17640=CARTESIAN_POINT('Ctrl Pts',(-1.54730100999696,0.159498697368912,
7.4445));
#17641=CARTESIAN_POINT('',(0.903606778650208,-1.26612599672284,0.));
#17642=CARTESIAN_POINT('Ctrl Pts',(0.903606778650207,-1.26612599672284,
-1.38777878078145E-15));
#17643=CARTESIAN_POINT('Ctrl Pts',(1.32452548910467,-0.965725403881512,
0.0370373134328344));
#17644=CARTESIAN_POINT('Ctrl Pts',(1.83597806077316,0.082627195836251,0.111111940298506));
#17645=CARTESIAN_POINT('Ctrl Pts',(0.924927935979477,1.59016247494986,0.222223880597014));
#17646=CARTESIAN_POINT('Ctrl Pts',(-0.833133967250649,1.63815181774712,
0.333335820895521));
#17647=CARTESIAN_POINT('Ctrl Pts',(-1.5310648992002,0.622568787117098,0.411242452161949));
#17648=CARTESIAN_POINT('Ctrl Pts',(-1.55772948793458,0.0543297678623362,
0.452111769995541));
#17649=CARTESIAN_POINT('Ctrl Pts',(-1.55735958542387,0.00101297198046621,
0.455943774396298));
#17650=CARTESIAN_POINT('Ctrl Pts',(0.863568564283469,1.75641400930303,0.));
#17651=CARTESIAN_POINT('Ctrl Pts',(0.902603531943078,1.7324423702308,2.28859211685802E-17));
#17652=CARTESIAN_POINT('Ctrl Pts',(0.940676776691071,1.70703651305647,-1.38032481715684E-16));
#17653=CARTESIAN_POINT('Ctrl Pts',(0.977697814042708,1.68019172043607,-1.28369537222284E-16));
#17654=CARTESIAN_POINT('Ctrl Pts',(1.03585714935899,1.63801906923031,-1.20927094907836E-16));
#17655=CARTESIAN_POINT('Ctrl Pts',(1.09142188330105,1.59229630788867,-2.7046412047637E-16));
#17656=CARTESIAN_POINT('Ctrl Pts',(1.14423064795477,1.54336420856895,-1.97758476261356E-16));
#17657=CARTESIAN_POINT('Ctrl Pts',(1.16946834979149,1.51997919396061,-1.63011907532148E-16));
#17658=CARTESIAN_POINT('Ctrl Pts',(1.19407597424497,1.49586072902399,-7.62289135782024E-17));
#17659=CARTESIAN_POINT('Ctrl Pts',(1.21803226410959,1.47104407323701,-6.59194920871187E-17));
#17660=CARTESIAN_POINT('Ctrl Pts',(1.23017793652576,1.45846220127952,-6.0692687062697E-17));
#17661=CARTESIAN_POINT('Ctrl Pts',(1.24215614940632,1.44570084965787,-2.95883426371776E-16));
#17662=CARTESIAN_POINT('Ctrl Pts',(1.25396388375076,1.43276453675822,-3.36536354339501E-16));
#17663=CARTESIAN_POINT('Ctrl Pts',(1.2638543668245,1.42192872524363,-3.70588365016071E-16));
#17664=CARTESIAN_POINT('Ctrl Pts',(1.2736185550329,1.41097745381189,1.09305947039191E-16));
#17665=CARTESIAN_POINT('Ctrl Pts',(1.28325381741352,1.39991535359824,9.71445146547012E-17));
#17666=CARTESIAN_POINT('Ctrl Pts',(1.33014189367208,1.34608385655041,3.79633375853411E-17));
#17667=CARTESIAN_POINT('Ctrl Pts',(1.37399192615748,1.28961736627304,-2.11573378166283E-16));
#17668=CARTESIAN_POINT('Ctrl Pts',(1.4146405205773,1.23085017638072,-2.98372437868011E-16));
#17669=CARTESIAN_POINT('Ctrl Pts',(1.44368223570237,1.18886348503472,-3.60386723994296E-16));
#17670=CARTESIAN_POINT('Ctrl Pts',(1.47108885988106,1.14570172941536,-3.55315850605615E-16));
#17671=CARTESIAN_POINT('Ctrl Pts',(1.49678522627473,1.10148200990233,-3.88578058618805E-16));
#17672=CARTESIAN_POINT('Ctrl Pts',(1.51163132719121,1.07593402353214,-4.0779533196023E-16));
#17673=CARTESIAN_POINT('Ctrl Pts',(1.52590630204136,1.05003284136309,-4.46468072791598E-16));
#17674=CARTESIAN_POINT('Ctrl Pts',(1.53959352057452,1.02380089191946,-4.5102810375397E-16));
#17675=CARTESIAN_POINT('Ctrl Pts',(1.54536419749809,1.0127412230066,-4.5295066131244E-16));
#17676=CARTESIAN_POINT('Ctrl Pts',(1.55102598614157,1.00163115224642,-3.28801907372083E-16));
#17677=CARTESIAN_POINT('Ctrl Pts',(1.55657733146951,0.990474109820403,-3.19189119579733E-16));
#17678=CARTESIAN_POINT('Ctrl Pts',(1.58759135376405,0.928142415050821,-2.65484801564386E-16));
#17679=CARTESIAN_POINT('Ctrl Pts',(1.61517084797965,0.864329379202861,-6.67259587666608E-16));
#17680=CARTESIAN_POINT('Ctrl Pts',(1.6391617363075,0.799343273084874,-5.82867087928207E-16));
#17681=CARTESIAN_POINT('Ctrl Pts',(1.66256147081466,0.735958474279834,-5.00554083870677E-16));
#17682=CARTESIAN_POINT('Ctrl Pts',(1.68254736306605,0.671456731546573,9.30631015772363E-17));
#17683=CARTESIAN_POINT('Ctrl Pts',(1.69892809919455,0.606119085630755,1.11022302462516E-16));
#17684=CARTESIAN_POINT('Ctrl Pts',(1.70969727271493,0.563164212250211,1.2282920473501E-16));
#17685=CARTESIAN_POINT('Ctrl Pts',(1.71890726464806,0.519847981128071,-1.31890518419189E-16));
#17686=CARTESIAN_POINT('Ctrl Pts',(1.72649157325935,0.476251973430995,-1.38777878078145E-16));
#17687=CARTESIAN_POINT('Ctrl Pts',(1.73286785345701,0.439599936333954,-1.44568219328534E-16));
#17688=CARTESIAN_POINT('Ctrl Pts',(1.73809492661148,0.402750145627894,-3.72078883249312E-16));
#17689=CARTESIAN_POINT('Ctrl Pts',(1.74212769993621,0.365752815321986,-4.16333634234434E-16));
#17690=CARTESIAN_POINT('Ctrl Pts',(1.74338298809393,0.354236593888137,-4.30108885249319E-16));
#17691=CARTESIAN_POINT('Ctrl Pts',(1.7445224615788,0.34270569873049,-4.2222380310258E-18));
#17692=CARTESIAN_POINT('Ctrl Pts',(1.74554359854572,0.331176868161872,-1.38777878078145E-17));
#17693=CARTESIAN_POINT('Ctrl Pts',(1.75129265664821,0.266268908759598,-6.82390718242887E-17));
#17694=CARTESIAN_POINT('Ctrl Pts',(1.75330855751176,0.201308359017101,-1.61972025925174E-16));
#17695=CARTESIAN_POINT('Ctrl Pts',(1.75142416657778,0.13655560768634,-1.38777878078145E-16));
#17696=CARTESIAN_POINT('Ctrl Pts',(1.75088156113035,0.117910222074166,-1.32099183788468E-16));
#17697=CARTESIAN_POINT('Ctrl Pts',(1.75001524326664,0.0992821075343112,
-1.58618989379829E-17));
#17698=CARTESIAN_POINT('Ctrl Pts',(1.74882042289714,0.0806776277944099,
0.));
#17699=CARTESIAN_POINT('Ctrl Pts',(1.74441970791246,0.0121543460832101,
6.07280452025807E-17));
#17700=CARTESIAN_POINT('Ctrl Pts',(1.735566761163,-0.0560504444942819,-6.11382253507945E-17));
#17701=CARTESIAN_POINT('Ctrl Pts',(1.72245455146386,-0.123599567095003,
-1.38777878078145E-16));
#17702=CARTESIAN_POINT('Ctrl Pts',(1.7106535204694,-0.184393995170097,-2.08653815792513E-16));
#17703=CARTESIAN_POINT('Ctrl Pts',(1.69540126258663,-0.244657625690558,
-3.30909447568271E-16));
#17704=CARTESIAN_POINT('Ctrl Pts',(1.67680583516799,-0.304119468797943,
-3.05311331771918E-16));
#17705=CARTESIAN_POINT('Ctrl Pts',(1.673496966793,-0.314700102829495,-3.00756405772578E-16));
#17706=CARTESIAN_POINT('Ctrl Pts',(1.67008375904048,-0.325250056291554,
1.12130257435328E-16));
#17707=CARTESIAN_POINT('Ctrl Pts',(1.66656954022458,-0.335760782955591,
1.11022302462516E-16));
#17708=CARTESIAN_POINT('Ctrl Pts',(1.64601748634937,-0.397230211008769,
1.04542697325368E-16));
#17709=CARTESIAN_POINT('Ctrl Pts',(1.62199078115275,-0.457436083404927,
4.89063387979405E-18));
#17710=CARTESIAN_POINT('Ctrl Pts',(1.59467603738004,-0.516104439016194,
-1.11022302462516E-16));
#17711=CARTESIAN_POINT('Ctrl Pts',(1.56746949320957,-0.574540396593861,
-2.26476082617573E-16));
#17712=CARTESIAN_POINT('Ctrl Pts',(1.53700015167997,-0.631451830043097,
-2.65447621135955E-16));
#17713=CARTESIAN_POINT('Ctrl Pts',(1.50341281573621,-0.68653552753498,-3.60822483003176E-16));
#17714=CARTESIAN_POINT('Ctrl Pts',(1.4705131167318,-0.740491490894733,-4.54244725638714E-16));
#17715=CARTESIAN_POINT('Ctrl Pts',(1.43462103920338,-0.792694411910378,
-4.2831431104574E-16));
#17716=CARTESIAN_POINT('Ctrl Pts',(1.39584581076301,-0.842817530414533,
-5.27355936696949E-16));
#17717=CARTESIAN_POINT('Ctrl Pts',(1.38890062306969,-0.851795284506205,
-5.45095682077361E-16));
#17718=CARTESIAN_POINT('Ctrl Pts',(1.38186288427344,-0.860706190744767,
2.35960662867998E-16));
#17719=CARTESIAN_POINT('Ctrl Pts',(1.37473315631241,-0.86954820289757,2.4980018054066E-16));
#17720=CARTESIAN_POINT('Ctrl Pts',(1.36794195322354,-0.877970389630667,
2.62982587454478E-16));
#17721=CARTESIAN_POINT('Ctrl Pts',(1.36107048536455,-0.886326025058287,
-6.35152333120316E-18));
#17722=CARTESIAN_POINT('Ctrl Pts',(1.35412452302825,-0.894607674989563,
0.));
#17723=CARTESIAN_POINT('Ctrl Pts',(1.31424959800426,-0.942150427756674,
3.64624085702422E-17));
#17724=CARTESIAN_POINT('Ctrl Pts',(1.2718724912058,-0.987319961554271,-3.18360401148313E-16));
#17725=CARTESIAN_POINT('Ctrl Pts',(1.22713193424969,-1.02984905091596,-2.22044604925031E-16));
#17726=CARTESIAN_POINT('Ctrl Pts',(1.18319618732353,-1.0716131109617,-1.27461373607439E-16));
#17727=CARTESIAN_POINT('Ctrl Pts',(1.13698054744349,-1.11083140282356,-2.10671899724563E-16));
#17728=CARTESIAN_POINT('Ctrl Pts',(1.08859303083371,-1.14720695088303,-2.77555756156289E-16));
#17729=CARTESIAN_POINT('Ctrl Pts',(1.04174975410163,-1.18242160919609,-3.42305080264122E-16));
#17730=CARTESIAN_POINT('Ctrl Pts',(0.992870408249348,-1.21497237243561,
-3.26158703430296E-16));
#17731=CARTESIAN_POINT('Ctrl Pts',(0.942040458977608,-1.24454244204819,
-3.60822483003176E-16));
#17732=CARTESIAN_POINT('Ctrl Pts',(0.92935042596986,-1.25192480549339,-3.69476524828035E-16));
#17733=CARTESIAN_POINT('Ctrl Pts',(0.916538776387811,-1.25912113789668,
-6.13893683198417E-17));
#17734=CARTESIAN_POINT('Ctrl Pts',(0.903606778650223,-1.26612599672282,
-5.55111512312578E-17));
#17735=CARTESIAN_POINT('Ctrl Pts',(0.0849160311154397,1.9485495525967,7.04599999999999));
#17736=CARTESIAN_POINT('Ctrl Pts',(0.400605874250757,1.93520776532856,7.0280673457103));
#17737=CARTESIAN_POINT('Ctrl Pts',(0.713151734000586,1.84952766933244,7.01013469142061));
#17738=CARTESIAN_POINT('Ctrl Pts',(0.983981247423036,1.69229543406338,6.99220203713092));
#17739=CARTESIAN_POINT('Ctrl Pts',(1.54334058226818,1.36755490846516,6.95516472369808));
#17740=CARTESIAN_POINT('Ctrl Pts',(1.92475070653735,0.737594779052165,6.91812741026524));
#17741=CARTESIAN_POINT('Ctrl Pts',(1.95488643500235,0.0915387903718514,
6.88109009683241));
#17742=CARTESIAN_POINT('Ctrl Pts',(1.98502216346735,-0.554517198308454,
6.84405278339957));
#17743=CARTESIAN_POINT('Ctrl Pts',(1.6638834961282,-1.21666904625608,6.80701546996674));
#17744=CARTESIAN_POINT('Ctrl Pts',(1.13779469346529,-1.59249087768303,6.7699781565339));
#17745=CARTESIAN_POINT('Ctrl Pts',(0.611705890802371,-1.96831270910999,
6.73294084310107));
#17746=CARTESIAN_POINT('Ctrl Pts',(-0.119333047184302,-2.05780452401628,
6.69590352966823));
#17747=CARTESIAN_POINT('Ctrl Pts',(-0.720597162266781,-1.81977576072458,
6.65886621623539));
#17748=CARTESIAN_POINT('Ctrl Pts',(-1.32186127734926,-1.58174699743288,
6.62182890280256));
#17749=CARTESIAN_POINT('Ctrl Pts',(-1.79335056952755,-1.0161976559432,6.58479158936972));
#17750=CARTESIAN_POINT('Ctrl Pts',(-1.91953678206301,-0.381975860707627,
6.54775427593688));
#17751=CARTESIAN_POINT('Ctrl Pts',(-1.94439039128642,-0.257059672615188,
6.540459414666));
#17752=CARTESIAN_POINT('Ctrl Pts',(-1.9558486040335,-0.129479463263859,
6.53316455339512));
#17753=CARTESIAN_POINT('Ctrl Pts',(-1.95467666345581,-0.00169153748172557,
6.52586969212423));
#17754=CARTESIAN_POINT('Origin',(0.,0.,-1.2940562256037));
#17755=CARTESIAN_POINT('',(-0.903606778650191,-1.26612599672285,1.38777878078145E-16));
#17756=CARTESIAN_POINT('Ctrl Pts',(-0.905552056217056,-1.26793026328003,
8.26433105977076E-16));
#17757=CARTESIAN_POINT('Ctrl Pts',(-0.513280080436939,-1.54506079646518,
0.0345343505799217));
#17758=CARTESIAN_POINT('Ctrl Pts',(0.58913651448779,-1.72157402054048,0.106143938272268));
#17759=CARTESIAN_POINT('Ctrl Pts',(1.77597071143275,-0.477272995959146,
0.214828763077039));
#17760=CARTESIAN_POINT('Ctrl Pts',(1.3630442868689,1.23477489449879,0.326054474414316));
#17761=CARTESIAN_POINT('Ctrl Pts',(-0.299513989741265,1.81437004394786,
0.437280185751592));
#17762=CARTESIAN_POINT('Ctrl Pts',(-1.41424275662139,0.944368549815884,
0.526614102814722));
#17763=CARTESIAN_POINT('Ctrl Pts',(-1.55418552513067,0.213449522874851,
0.578872782765425));
#17764=CARTESIAN_POINT('Ctrl Pts',(-1.55327638232574,0.000749985450955847,
0.594056225603703));
#17765=CARTESIAN_POINT('Origin',(0.,0.,0.));
#17766=CARTESIAN_POINT('Ctrl Pts',(-0.685825729128727,1.39614588036675,
-0.230074082272066));
#17767=CARTESIAN_POINT('Ctrl Pts',(-1.15044430012221,1.1679123019855,-0.19299884515964));
#17768=CARTESIAN_POINT('Ctrl Pts',(-1.8258407957124,0.215070471435756,-0.118848370934789));
#17769=CARTESIAN_POINT('Ctrl Pts',(-1.16856980438922,-1.42158824274557,
-0.0076226595975132));
#17770=CARTESIAN_POINT('Ctrl Pts',(0.561390129169046,-1.75066389321976,
0.103603051739764));
#17771=CARTESIAN_POINT('Ctrl Pts',(1.77597071143275,-0.477272995959146,
0.214828763077039));
#17772=CARTESIAN_POINT('Ctrl Pts',(1.3630442868689,1.23477489449879,0.326054474414316));
#17773=CARTESIAN_POINT('Ctrl Pts',(-0.299513989741265,1.81437004394786,
0.437280185751592));
#17774=CARTESIAN_POINT('Ctrl Pts',(-1.68741350339127,0.731169639996686,
0.548505897088869));
#17775=CARTESIAN_POINT('Ctrl Pts',(-1.52862817745114,-1.02241621535808,
0.659731608426144));
#17776=CARTESIAN_POINT('Ctrl Pts',(0.0313843551128396,-1.83872969125081,
0.770957319763422));
#17777=CARTESIAN_POINT('Ctrl Pts',(1.56261245507102,-0.969643437172017,
0.882183031100698));
#17778=CARTESIAN_POINT('Ctrl Pts',(1.66150197094076,0.788277540412492,0.993408742437974));
#17779=CARTESIAN_POINT('Ctrl Pts',(0.237394066880885,1.82362194812979,1.10463445377525));
#17780=CARTESIAN_POINT('Ctrl Pts',(-1.40431546877471,1.18737513564603,1.21586016511253));
#17781=CARTESIAN_POINT('Ctrl Pts',(-1.75877981175223,-0.537266275957094,
1.3270858764498));
#17782=CARTESIAN_POINT('Ctrl Pts',(-0.501082205369057,-1.76942810040879,
1.43831158778708));
#17783=CARTESIAN_POINT('Ctrl Pts',(1.21592516185098,-1.37966899434435,1.54953729912436));
#17784=CARTESIAN_POINT('Ctrl Pts',(1.8183716526183,0.274745208061178,1.66076301046163));
#17785=CARTESIAN_POINT('Ctrl Pts',(0.754032712405612,1.67731773070425,1.77198872179891));
#17786=CARTESIAN_POINT('Ctrl Pts',(-1.00147988107901,1.54240019271928,1.88321443313619));
#17787=CARTESIAN_POINT('Ctrl Pts',(-1.83899975790172,-0.00633731701985082,
1.99444014447346));
#17788=CARTESIAN_POINT('Ctrl Pts',(-0.990825815880477,-1.5492657736205,
2.10566585581074));
#17789=CARTESIAN_POINT('Ctrl Pts',(0.765574959497512,-1.6720811124538,2.21689156714802));
#17790=CARTESIAN_POINT('Ctrl Pts',(1.82022199392772,-0.262206313316451,
2.32811727848529));
#17791=CARTESIAN_POINT('Ctrl Pts',(1.20638759997596,1.38801628675575,2.43934298982257));
#17792=CARTESIAN_POINT('Ctrl Pts',(-0.513265374585843,1.76593287340023,
2.55056870115984));
#17793=CARTESIAN_POINT('Ctrl Pts',(-1.76244071170529,0.525131406868061,
2.66179441249712));
#17794=CARTESIAN_POINT('Ctrl Pts',(-1.39609903883734,-1.19702453193727,
2.77302012383439));
#17795=CARTESIAN_POINT('Ctrl Pts',(0.249957593646744,-1.82194441691009,
2.88424583517168));
#17796=CARTESIAN_POINT('Ctrl Pts',(1.6668940398915,-0.776804039943688,2.99547154650895));
#17797=CARTESIAN_POINT('Ctrl Pts',(1.55589501744036,0.980383063583733,3.10669725784622));
#17798=CARTESIAN_POINT('Ctrl Pts',(0.0187062518377651,1.83891553174339,
3.2179229691835));
#17799=CARTESIAN_POINT('Ctrl Pts',(-1.53562934193987,1.01183139943408,3.32914868052078));
#17800=CARTESIAN_POINT('Ctrl Pts',(-1.68235144492823,-0.742734052303713,
3.44037439185806));
#17801=CARTESIAN_POINT('Ctrl Pts',(-0.286969261786828,-1.81648256240041,
3.55160010319533));
#17802=CARTESIAN_POINT('Ctrl Pts',(1.37145934362907,-1.22517734450477,3.66282581453261));
#17803=CARTESIAN_POINT('Ctrl Pts',(1.77275862659963,0.489169815626649,3.77405152586988));
#17804=CARTESIAN_POINT('Ctrl Pts',(0.549083125265984,1.75512620009375,3.88527723720716));
#17805=CARTESIAN_POINT('Ctrl Pts',(-1.17790186202284,1.41227032121617,3.99650294854444));
#17806=CARTESIAN_POINT('Ctrl Pts',(-1.82517932708368,-0.225123700760077,
4.10772865988171));
#17807=CARTESIAN_POINT('Ctrl Pts',(-0.799431294618187,-1.65616118233816,
4.21895437121899));
#17808=CARTESIAN_POINT('Ctrl Pts',(0.959104426053338,-1.56910132141185,
4.33018008255627));
#17809=CARTESIAN_POINT('Ctrl Pts',(1.83849028118038,-0.0437463405035559,
4.44140579389354));
#17810=CARTESIAN_POINT('Ctrl Pts',(1.0326493363287,1.52170812080878,4.55263150523082));
#17811=CARTESIAN_POINT('Ctrl Pts',(-0.719755403894915,1.69230978744094,
4.6638572165681));
#17812=CARTESIAN_POINT('Ctrl Pts',(-1.81240626272056,0.311678989548955,
4.77508292790537));
#17813=CARTESIAN_POINT('Ctrl Pts',(-1.24373988019232,-1.35464806069341,
4.88630863924265));
#17814=CARTESIAN_POINT('Ctrl Pts',(0.464983542380115,-1.77925562259896,
4.99753435057992));
#17815=CARTESIAN_POINT('Ctrl Pts',(1.74748619395055,-0.572933012383953,
5.1087600619172));
#17816=CARTESIAN_POINT('Ctrl Pts',(1.42817970701863,1.15856074316792,5.21998577325448));
#17817=CARTESIAN_POINT('Ctrl Pts',(-0.20024807751692,1.82807576816643,5.33121148459175));
#17818=CARTESIAN_POINT('Ctrl Pts',(-1.64512115233065,0.821910272029074,
5.44243719592903));
#17819=CARTESIAN_POINT('Ctrl Pts',(-1.58201670345687,-0.937647879740503,
5.55366290726631));
#17820=CARTESIAN_POINT('Ctrl Pts',(-0.0687781849042931,-1.83772416168987,
5.66488861860358));
#17821=CARTESIAN_POINT('Ctrl Pts',(1.50750444735784,-1.05327561457109,5.77611432994086));
#17822=CARTESIAN_POINT('Ctrl Pts',(1.70195476716013,0.696642984640571,5.88734004127814));
#17823=CARTESIAN_POINT('Ctrl Pts',(0.336330007005007,1.80799440678846,5.99856575261541));
#17824=CARTESIAN_POINT('Ctrl Pts',(-1.33758382509627,1.26207070464844,6.10979146395269));
#17825=CARTESIAN_POINT('Ctrl Pts',(-1.78542595464098,-0.440709020390059,
6.22101717528996));
#17826=CARTESIAN_POINT('Ctrl Pts',(-0.59667036110871,-1.73952595846347,
6.33224288662724));
#17827=CARTESIAN_POINT('Ctrl Pts',(1.13899278941852,-1.44381691390763,6.44346859796452));
#17828=CARTESIAN_POINT('Ctrl Pts',(1.83065601360088,0.17532136832598,6.5546943093018));
#17829=CARTESIAN_POINT('Ctrl Pts',(0.844193344579619,1.63380261073593,6.66592002063907));
#17830=CARTESIAN_POINT('Ctrl Pts',(-0.915934603694247,1.5945880622222,6.77714573197635));
#17831=CARTESIAN_POINT('Ctrl Pts',(-1.83677508915277,0.093893769326276,
6.88837144331362));
#17832=CARTESIAN_POINT('Ctrl Pts',(-1.07340561084952,-1.49320523543669,
6.99959715465089));
#17833=CARTESIAN_POINT('Ctrl Pts',(0.672826183539381,-1.71093187207897,
7.11082286598819));
#17834=CARTESIAN_POINT('Ctrl Pts',(1.80435891657647,-0.361603954366771,
7.22204857732544));
#17835=CARTESIAN_POINT('Ctrl Pts',(1.27791236939833,1.32169962363241,7.33327428866273));
#17836=CARTESIAN_POINT('Ctrl Pts',(0.152038852759137,1.63230677878407,7.40742476288758));
#17837=CARTESIAN_POINT('Ctrl Pts',(-0.352169241380528,1.51510959188617,
7.44450000000001));
#17838=CARTESIAN_POINT('Ctrl Pts',(-0.744392439309327,1.51537102412035,
-0.153382721514711));
#17839=CARTESIAN_POINT('Ctrl Pts',(-1.24868753458029,1.26764723230613,-0.116307484402285));
#17840=CARTESIAN_POINT('Ctrl Pts',(-1.9817601264938,0.233436609412224,-0.042157010177434));
#17841=CARTESIAN_POINT('Ctrl Pts',(-1.26836088272398,-1.54298606011064,
0.0690687011598421));
#17842=CARTESIAN_POINT('Ctrl Pts',(0.609330548428412,-1.9001634242276,0.180294412497119));
#17843=CARTESIAN_POINT('Ctrl Pts',(1.92763134113508,-0.518030156334108,
0.291520123834394));
#17844=CARTESIAN_POINT('Ctrl Pts',(1.47944269002272,1.34021961655124,0.402745835171672));
#17845=CARTESIAN_POINT('Ctrl Pts',(-0.325091258553406,1.96930981947839,
0.513971546508948));
#17846=CARTESIAN_POINT('Ctrl Pts',(-1.8315117099918,0.793608534572646,0.625197257846224));
#17847=CARTESIAN_POINT('Ctrl Pts',(-1.65916676712527,-1.10972637539669,
0.7364229691835));
#17848=CARTESIAN_POINT('Ctrl Pts',(0.0340644505831978,-1.9957496809569,
0.847648680520777));
#17849=CARTESIAN_POINT('Ctrl Pts',(1.69605316295611,-1.05244701795271,0.958874391858054));
#17850=CARTESIAN_POINT('Ctrl Pts',(1.80338743872602,0.855593215941119,1.07010010319533));
#17851=CARTESIAN_POINT('Ctrl Pts',(0.257666548537818,1.97935179840939,1.18132581453261));
#17852=CARTESIAN_POINT('Ctrl Pts',(-1.52423826194019,1.28877211229984,1.29255152586988));
#17853=CARTESIAN_POINT('Ctrl Pts',(-1.90897240898426,-0.583146616891169,
1.40377723720716));
#17854=CARTESIAN_POINT('Ctrl Pts',(-0.543872574776452,-1.9205300179086,
1.51500294854444));
#17855=CARTESIAN_POINT('Ctrl Pts',(1.31976019388731,-1.49748707947159,1.62622865988171));
#17856=CARTESIAN_POINT('Ctrl Pts',(1.97365314915069,0.298207324296545,1.73745437121899));
#17857=CARTESIAN_POINT('Ctrl Pts',(0.818424019786662,1.82055379963935,1.84868008255626));
#17858=CARTESIAN_POINT('Ctrl Pts',(-1.08700216386266,1.6741148561284,1.95990579389354));
#17859=CARTESIAN_POINT('Ctrl Pts',(-1.99604281019441,-0.00687849795467773,
2.07113150523082));
#17860=CARTESIAN_POINT('Ctrl Pts',(-1.07543828510332,-1.68156672953773,
2.1823572165681));
#17861=CARTESIAN_POINT('Ctrl Pts',(0.830951927537738,-1.81486999562381,
2.29358292790537));
#17862=CARTESIAN_POINT('Ctrl Pts',(1.97566150203448,-0.284597659262374,
2.40480863924265));
#17863=CARTESIAN_POINT('Ctrl Pts',(1.30940816326546,1.50654719648941,2.51603435057992));
#17864=CARTESIAN_POINT('Ctrl Pts',(-0.557096136778581,1.91673631281949,
2.6272600619172));
#17865=CARTESIAN_POINT('Ctrl Pts',(-1.91294593480924,0.569975479650009,
2.73848577325448));
#17866=CARTESIAN_POINT('Ctrl Pts',(-1.51532018251605,-1.29924552753932,
2.84971148459175));
#17867=CARTESIAN_POINT('Ctrl Pts',(0.271302949066904,-1.97753101288966,
2.96093719592903));
#17868=CARTESIAN_POINT('Ctrl Pts',(1.80923996829539,-0.843139925493371,
3.0721629072663));
#17869=CARTESIAN_POINT('Ctrl Pts',(1.6887620836463,1.06410376450264,3.18338861860358));
#17870=CARTESIAN_POINT('Ctrl Pts',(0.0203036891799667,1.9959513914669,3.29461432994085));
#17871=CARTESIAN_POINT('Ctrl Pts',(-1.66676580240553,1.09823765951648,3.40584004127814));
#17872=CARTESIAN_POINT('Ctrl Pts',(-1.82601737245506,-0.806160500357498,
3.51706575261541));
#17873=CARTESIAN_POINT('Ctrl Pts',(-0.31147526217729,-1.97160273836024,
3.6282914639527));
#17874=CARTESIAN_POINT('Ctrl Pts',(1.48857635818734,-1.32980247507055,3.73951717528996));
#17875=CARTESIAN_POINT('Ctrl Pts',(1.92414495740429,0.530942915707476,3.85074288662724));
#17876=CARTESIAN_POINT('Ctrl Pts',(0.595972576764652,1.90500679384439,3.96196859796451));
#17877=CARTESIAN_POINT('Ctrl Pts',(-1.27848985988335,1.53287242622092,4.07319430930179));
#17878=CARTESIAN_POINT('Ctrl Pts',(-1.98104217115158,-0.244348343372923,
4.18442002063907));
#17879=CARTESIAN_POINT('Ctrl Pts',(-0.867699455103643,-1.79759056863662,
4.29564573197634));
#17880=CARTESIAN_POINT('Ctrl Pts',(1.04100801842068,-1.70309615192351,4.40687144331362));
#17881=CARTESIAN_POINT('Ctrl Pts',(1.99548982624636,-0.047482098928651,
4.5180971546509));
#17882=CARTESIAN_POINT('Ctrl Pts',(1.12083336301401,1.65165576596945,4.62932286598818));
#17883=CARTESIAN_POINT('Ctrl Pts',(-0.781219569426276,1.83682611665882,
4.74054857732545));
#17884=CARTESIAN_POINT('Ctrl Pts',(-1.96717833937204,0.338295099553305,
4.85177428866273));
#17885=CARTESIAN_POINT('Ctrl Pts',(-1.34995017532929,-1.47032946049761,
4.963));
#17886=CARTESIAN_POINT('Ctrl Pts',(0.504691233720185,-1.93119677026974,
5.07422571133729));
#17887=CARTESIAN_POINT('Ctrl Pts',(1.89671436244713,-0.621859146624829,
5.18545142267455));
#17888=CARTESIAN_POINT('Ctrl Pts',(1.55014040845374,1.25749708864148,5.29667713401184));
#17889=CARTESIAN_POINT('Ctrl Pts',(-0.217348443720809,1.98418595644765,
5.4079028453491));
#17890=CARTESIAN_POINT('Ctrl Pts',(-1.78560776525334,0.892098045178891,
5.5191285566864));
#17891=CARTESIAN_POINT('Ctrl Pts',(-1.71711445473246,-1.01771917087445,
5.63035426802365));
#17892=CARTESIAN_POINT('Ctrl Pts',(-0.0746515603857894,-1.99465828328709,
5.74157997936095));
#17893=CARTESIAN_POINT('Ctrl Pts',(1.63623915694148,-1.14322104099488,5.85280569069821));
#17894=CARTESIAN_POINT('Ctrl Pts',(1.84729473816909,0.756133444166813,5.96403140203549));
#17895=CARTESIAN_POINT('Ctrl Pts',(0.365051213003408,1.96238972900109,6.07525711337277));
#17896=CARTESIAN_POINT('Ctrl Pts',(-1.45180800902444,1.36984637716583,6.18648282471005));
#17897=CARTESIAN_POINT('Ctrl Pts',(-1.93789402341296,-0.478343766907873,
6.29770853604731));
#17898=CARTESIAN_POINT('Ctrl Pts',(-0.647623567773631,-1.88807435543072,
6.4089342473846));
#17899=CARTESIAN_POINT('Ctrl Pts',(1.23625811173359,-1.56711296880792,6.52015995872187));
#17900=CARTESIAN_POINT('Ctrl Pts',(1.98698654428125,0.190293095590063,6.63138567005915));
#17901=CARTESIAN_POINT('Ctrl Pts',(0.916284000920563,1.77332266653327,6.74261138139642));
#17902=CARTESIAN_POINT('Ctrl Pts',(-0.994151669926352,1.73075935608174,
6.8538370927337));
#17903=CARTESIAN_POINT('Ctrl Pts',(-1.99362816383988,0.101911912919242,
6.96506280407097));
#17904=CARTESIAN_POINT('Ctrl Pts',(-1.16507005656334,-1.62071885084899,
7.07628851540826));
#17905=CARTESIAN_POINT('Ctrl Pts',(0.730282785733831,-1.85703845110468,
7.18751422674552));
#17906=CARTESIAN_POINT('Ctrl Pts',(1.95844378280506,-0.392483452023516,
7.29873993808281));
#17907=CARTESIAN_POINT('Ctrl Pts',(1.38704085524538,1.43456736176966,7.40996564942008));
#17908=CARTESIAN_POINT('Ctrl Pts',(0.165022348489246,1.77169909665516,7.48411612364493));
#17909=CARTESIAN_POINT('Ctrl Pts',(-0.382243053164543,1.64449374968465,
7.52119136075736));
#17910=CARTESIAN_POINT('Ctrl Pts',(-0.802959149489926,1.63459616787395,
-0.0766913607573553));
#17911=CARTESIAN_POINT('Ctrl Pts',(-1.34693076903838,1.36738216262677,-0.0396161236449298));
#17912=CARTESIAN_POINT('Ctrl Pts',(-2.1376794572752,0.251802747388692,0.034534350579921));
#17913=CARTESIAN_POINT('Ctrl Pts',(-1.36815196105874,-1.66438387747571,
0.145760061917198));
#17914=CARTESIAN_POINT('Ctrl Pts',(0.657270967687777,-2.04966295523545,
0.256985773254474));
#17915=CARTESIAN_POINT('Ctrl Pts',(2.07929197083741,-0.558787316709069,
0.36821148459175));
#17916=CARTESIAN_POINT('Ctrl Pts',(1.59584109317654,1.44566433860368,0.479437195929027));
#17917=CARTESIAN_POINT('Ctrl Pts',(-0.350668527365547,2.12424959500892,
0.590662907266303));
#17918=CARTESIAN_POINT('Ctrl Pts',(-1.97560991659234,0.856047429148608,
0.70188861860358));
#17919=CARTESIAN_POINT('Ctrl Pts',(-1.7897053567994,-1.1970365354353,0.813114329940855));
#17920=CARTESIAN_POINT('Ctrl Pts',(0.0367445460535571,-2.15276967066298,
0.924340041278132));
#17921=CARTESIAN_POINT('Ctrl Pts',(1.8294938708412,-1.13525059873339,1.03556575261541));
#17922=CARTESIAN_POINT('Ctrl Pts',(1.94527290651128,0.922908891469747,1.14679146395268));
#17923=CARTESIAN_POINT('Ctrl Pts',(0.277939030194749,2.13508164868898,1.25801717528996));
#17924=CARTESIAN_POINT('Ctrl Pts',(-1.64416105510567,1.39016908895364,1.36924288662724));
#17925=CARTESIAN_POINT('Ctrl Pts',(-2.05916500621629,-0.629026957825243,
1.48046859796451));
#17926=CARTESIAN_POINT('Ctrl Pts',(-0.586662944183848,-2.07163193540842,
1.59169430930179));
#17927=CARTESIAN_POINT('Ctrl Pts',(1.42359522592366,-1.61530516459883,1.70292002063907));
#17928=CARTESIAN_POINT('Ctrl Pts',(2.12893464568308,0.32166944053191,1.81414573197634));
#17929=CARTESIAN_POINT('Ctrl Pts',(0.882815327167714,1.96378986857444,1.92537144331362));
#17930=CARTESIAN_POINT('Ctrl Pts',(-1.17252444664632,1.80582951953752,2.0365971546509));
#17931=CARTESIAN_POINT('Ctrl Pts',(-2.1530858624871,-0.00741967888950297,
2.14782286598817));
#17932=CARTESIAN_POINT('Ctrl Pts',(-1.16005075432617,-1.81386768545496,
2.25904857732545));
#17933=CARTESIAN_POINT('Ctrl Pts',(0.896328895577965,-1.95765887879382,
2.37027428866273));
#17934=CARTESIAN_POINT('Ctrl Pts',(2.13110101014124,-0.306989005208296,
2.4815));
#17935=CARTESIAN_POINT('Ctrl Pts',(1.41242872655496,1.62507810622307,2.59272571133728));
#17936=CARTESIAN_POINT('Ctrl Pts',(-0.600926898971321,2.06753975223876,
2.70395142267456));
#17937=CARTESIAN_POINT('Ctrl Pts',(-2.06345115791318,0.614819552431958,
2.81517713401183));
#17938=CARTESIAN_POINT('Ctrl Pts',(-1.63454132619476,-1.40146652314137,
2.92640284534911));
#17939=CARTESIAN_POINT('Ctrl Pts',(0.292648304487066,-2.13311760886924,
3.03762855668638));
#17940=CARTESIAN_POINT('Ctrl Pts',(1.95158589669928,-0.909475811043054,
3.14885426802366));
#17941=CARTESIAN_POINT('Ctrl Pts',(1.82162914985223,1.14782446542155,3.26007997936093));
#17942=CARTESIAN_POINT('Ctrl Pts',(0.021901126522171,2.15298725119041,3.37130569069822));
#17943=CARTESIAN_POINT('Ctrl Pts',(-1.79790226287119,1.18464391959888,3.48253140203548));
#17944=CARTESIAN_POINT('Ctrl Pts',(-1.96968329998188,-0.869586948411284,
3.59375711337277));
#17945=CARTESIAN_POINT('Ctrl Pts',(-0.335981262567754,-2.12672291432008,
3.70498282471004));
#17946=CARTESIAN_POINT('Ctrl Pts',(1.60569337274561,-1.43442760563632,3.81620853604732));
#17947=CARTESIAN_POINT('Ctrl Pts',(2.07553128820896,0.572716015788303,3.9274342473846));
#17948=CARTESIAN_POINT('Ctrl Pts',(0.642862028263319,2.05488738759502,4.03865995872187));
#17949=CARTESIAN_POINT('Ctrl Pts',(-1.37907785774386,1.65347453122567,4.14988567005915));
#17950=CARTESIAN_POINT('Ctrl Pts',(-2.13690501521948,-0.263572985985768,
4.26111138139642));
#17951=CARTESIAN_POINT('Ctrl Pts',(-0.935967615589101,-1.93901995493508,
4.3723370927337));
#17952=CARTESIAN_POINT('Ctrl Pts',(1.12291161078803,-1.83709098243517,4.48356280407097));
#17953=CARTESIAN_POINT('Ctrl Pts',(2.15248937131234,-0.0512178573537473,
4.59478851540826));
#17954=CARTESIAN_POINT('Ctrl Pts',(1.20901738969933,1.78160341113012,4.70601422674553));
#17955=CARTESIAN_POINT('Ctrl Pts',(-0.842683734957634,1.9813424458767,4.81723993808281));
#17956=CARTESIAN_POINT('Ctrl Pts',(-2.12195041602352,0.364911209557656,
4.92846564942008));
#17957=CARTESIAN_POINT('Ctrl Pts',(-1.45616047046626,-1.58601086030181,
5.03969136075736));
#17958=CARTESIAN_POINT('Ctrl Pts',(0.544398925060255,-2.08313791794051,
5.15091707209464));
#17959=CARTESIAN_POINT('Ctrl Pts',(2.04594253094371,-0.670785280865706,
5.26214278343191));
#17960=CARTESIAN_POINT('Ctrl Pts',(1.67210110988885,1.35643343411504,5.37336849476919));
#17961=CARTESIAN_POINT('Ctrl Pts',(-0.234448809924699,2.14029614472887,
5.48459420610646));
#17962=CARTESIAN_POINT('Ctrl Pts',(-1.92609437817603,0.96228581832871,5.59581991744374));
#17963=CARTESIAN_POINT('Ctrl Pts',(-1.85221220600806,-1.09779046200839,
5.70704562878101));
#17964=CARTESIAN_POINT('Ctrl Pts',(-0.0805249358672843,-2.15159240488431,
5.8182713401183));
#17965=CARTESIAN_POINT('Ctrl Pts',(1.76497386652513,-1.23316646741867,5.92949705145556));
#17966=CARTESIAN_POINT('Ctrl Pts',(1.99263470917806,0.815623903693059,6.04072276279285));
#17967=CARTESIAN_POINT('Ctrl Pts',(0.393772419001808,2.11678505121371,6.15194847413012));
#17968=CARTESIAN_POINT('Ctrl Pts',(-1.56603219295262,1.47762204968323,6.2631741854674));
#17969=CARTESIAN_POINT('Ctrl Pts',(-2.09036209218494,-0.515978513425692,
6.37439989680467));
#17970=CARTESIAN_POINT('Ctrl Pts',(-0.698576774438554,-2.03662275239797,
6.48562560814195));
#17971=CARTESIAN_POINT('Ctrl Pts',(1.33352343404865,-1.69040902370822,6.59685131947923));
#17972=CARTESIAN_POINT('Ctrl Pts',(2.14331707496162,0.205264822854154,6.70807703081651));
#17973=CARTESIAN_POINT('Ctrl Pts',(0.988374657261507,1.9128427223306,6.81930274215378));
#17974=CARTESIAN_POINT('Ctrl Pts',(-1.07236873615846,1.86693064994129,6.93052845349106));
#17975=CARTESIAN_POINT('Ctrl Pts',(-2.15048123852699,0.109930056512203,
7.04175416482834));
#17976=CARTESIAN_POINT('Ctrl Pts',(-1.25673450227717,-1.74823246626129,
7.1529798761656));
#17977=CARTESIAN_POINT('Ctrl Pts',(0.787739387928281,-2.00314503013039,
7.26420558750289));
#17978=CARTESIAN_POINT('Ctrl Pts',(2.11252864903365,-0.42336294968026,7.37543129884016));
#17979=CARTESIAN_POINT('Ctrl Pts',(1.49616934109244,1.54743509990691,7.48665701017744));
#17980=CARTESIAN_POINT('Ctrl Pts',(0.178005844219355,1.91109141452625,7.56080748440229));
#17981=CARTESIAN_POINT('Ctrl Pts',(-0.412316864948557,1.77387790748314,
7.59788272151472));
#17982=CARTESIAN_POINT('Ctrl Pts',(-0.861525859670525,1.75382131162755,
0.));
#17983=CARTESIAN_POINT('Ctrl Pts',(-1.44517400349647,1.4671170929474,0.0370752371124254));
#17984=CARTESIAN_POINT('Ctrl Pts',(-2.29359878805659,0.270168885365161,
0.111225711337276));
#17985=CARTESIAN_POINT('Ctrl Pts',(-1.46794303939349,-1.78578169484077,
0.222451422674553));
#17986=CARTESIAN_POINT('Ctrl Pts',(0.705211386947141,-2.19916248624329,
0.33367713401183));
#17987=CARTESIAN_POINT('Ctrl Pts',(2.23095260053975,-0.599544477084032,
0.444902845349104));
#17988=CARTESIAN_POINT('Ctrl Pts',(1.71223949633035,1.55110906065613,0.556128556686383));
#17989=CARTESIAN_POINT('Ctrl Pts',(-0.376245796177686,2.27918937053945,
0.667354268023658));
#17990=CARTESIAN_POINT('Ctrl Pts',(-2.11970812319287,0.918486323724569,
0.778579979360935));
#17991=CARTESIAN_POINT('Ctrl Pts',(-1.92024394647352,-1.28434669547391,
0.889805690698211));
#17992=CARTESIAN_POINT('Ctrl Pts',(0.0394246415239131,-2.30978966036907,
1.00103140203549));
#17993=CARTESIAN_POINT('Ctrl Pts',(1.96293457872629,-1.21805417951409,1.11225711337277));
#17994=CARTESIAN_POINT('Ctrl Pts',(2.08715837429654,0.990224566998375,1.22348282471004));
#17995=CARTESIAN_POINT('Ctrl Pts',(0.298211511851683,2.29081149896857,1.33470853604732));
#17996=CARTESIAN_POINT('Ctrl Pts',(-1.76408384827114,1.49156606560744,1.44593424738459));
#17997=CARTESIAN_POINT('Ctrl Pts',(-2.20935760344832,-0.674907298759319,
1.55715995872187));
#17998=CARTESIAN_POINT('Ctrl Pts',(-0.629453313591242,-2.22273385290824,
1.66838567005915));
#17999=CARTESIAN_POINT('Ctrl Pts',(1.52743025795999,-1.73312324972607,1.77961138139642));
#18000=CARTESIAN_POINT('Ctrl Pts',(2.28421614221547,0.345131556767278,1.8908370927337));
#18001=CARTESIAN_POINT('Ctrl Pts',(0.947206634548765,2.10702593750954,2.00206280407097));
#18002=CARTESIAN_POINT('Ctrl Pts',(-1.25804672942998,1.93754418294664,2.11328851540825));
#18003=CARTESIAN_POINT('Ctrl Pts',(-2.31012891477979,-0.0079608598243287,
2.22451422674552));
#18004=CARTESIAN_POINT('Ctrl Pts',(-1.24466322354901,-1.94616864137219,
2.33573993808281));
#18005=CARTESIAN_POINT('Ctrl Pts',(0.961705863618192,-2.10044776196383,
2.44696564942008));
#18006=CARTESIAN_POINT('Ctrl Pts',(2.286540518248,-0.329380351154219,2.55819136075736));
#18007=CARTESIAN_POINT('Ctrl Pts',(1.51544928984446,1.74360901595674,2.66941707209463));
#18008=CARTESIAN_POINT('Ctrl Pts',(-0.644757661164061,2.21834319165802,
2.78064278343191));
#18009=CARTESIAN_POINT('Ctrl Pts',(-2.21395638101712,0.659663625213907,
2.89186849476918));
#18010=CARTESIAN_POINT('Ctrl Pts',(-1.75376246987347,-1.50368751874342,
3.00309420610647));
#18011=CARTESIAN_POINT('Ctrl Pts',(0.313993659907229,-2.28870420484881,
3.11431991744373));
#18012=CARTESIAN_POINT('Ctrl Pts',(2.09393182510317,-0.975811696592738,
3.22554562878102));
#18013=CARTESIAN_POINT('Ctrl Pts',(1.95449621605817,1.23154516634045,3.33677134011829));
#18014=CARTESIAN_POINT('Ctrl Pts',(0.0234985638643735,2.31002311091391,
3.44799705145557));
#18015=CARTESIAN_POINT('Ctrl Pts',(-1.92903872333685,1.27105017968128,3.55922276279284));
#18016=CARTESIAN_POINT('Ctrl Pts',(-2.1133492275087,-0.93301339646507,3.67044847413012));
#18017=CARTESIAN_POINT('Ctrl Pts',(-0.360487262958215,-2.28184309027991,
3.7816741854674));
#18018=CARTESIAN_POINT('Ctrl Pts',(1.72281038730387,-1.53905273620209,3.89289989680467));
#18019=CARTESIAN_POINT('Ctrl Pts',(2.22691761901362,0.614489115869131,4.00412560814195));
#18020=CARTESIAN_POINT('Ctrl Pts',(0.689751479761988,2.20476798134566,4.11535131947922));
#18021=CARTESIAN_POINT('Ctrl Pts',(-1.47966585560437,1.77407663623043,4.22657703081651));
#18022=CARTESIAN_POINT('Ctrl Pts',(-2.29276785928738,-0.282797628598616,
4.33780274215377));
#18023=CARTESIAN_POINT('Ctrl Pts',(-1.00423577607456,-2.08044934123353,
4.44902845349105));
#18024=CARTESIAN_POINT('Ctrl Pts',(1.20481520315537,-1.97108581294683,4.56025416482834));
#18025=CARTESIAN_POINT('Ctrl Pts',(2.30948891637831,-0.0549536157788429,
4.6714798761656));
#18026=CARTESIAN_POINT('Ctrl Pts',(1.29720141638464,1.91155105629079,4.78270558750289));
#18027=CARTESIAN_POINT('Ctrl Pts',(-0.904147900488994,2.12585877509457,
4.89393129884016));
#18028=CARTESIAN_POINT('Ctrl Pts',(-2.276722492675,0.391527319562006,5.00515701017744));
#18029=CARTESIAN_POINT('Ctrl Pts',(-1.56237076560323,-1.701692260106,5.11638272151471));
#18030=CARTESIAN_POINT('Ctrl Pts',(0.584106616400323,-2.2350790656113,5.227608432852));
#18031=CARTESIAN_POINT('Ctrl Pts',(2.19517069944029,-0.71971141510658,5.33883414418926));
#18032=CARTESIAN_POINT('Ctrl Pts',(1.79406181132396,1.4553697795886,5.45005985552654));
#18033=CARTESIAN_POINT('Ctrl Pts',(-0.251549176128587,2.2964063330101,5.56128556686382));
#18034=CARTESIAN_POINT('Ctrl Pts',(-2.06658099109872,1.03247359147853,5.6725112782011));
#18035=CARTESIAN_POINT('Ctrl Pts',(-1.98730995728366,-1.17786175314234,
5.78373698953836));
#18036=CARTESIAN_POINT('Ctrl Pts',(-0.0863983113487825,-2.30852652648153,
5.89496270087566));
#18037=CARTESIAN_POINT('Ctrl Pts',(1.89370857610877,-1.32311189384246,6.00618841221292));
#18038=CARTESIAN_POINT('Ctrl Pts',(2.13797468018702,0.875114363219305,6.1174141235502));
#18039=CARTESIAN_POINT('Ctrl Pts',(0.422493625000208,2.27118037342633,6.22863983488748));
#18040=CARTESIAN_POINT('Ctrl Pts',(-1.68025637688079,1.58539772220062,6.33986554622475));
#18041=CARTESIAN_POINT('Ctrl Pts',(-2.24283016095692,-0.55361325994351,
6.45109125756204));
#18042=CARTESIAN_POINT('Ctrl Pts',(-0.749529981103475,-2.18517114936522,
6.56231696889931));
#18043=CARTESIAN_POINT('Ctrl Pts',(1.43078875636371,-1.81370507860851,6.67354268023658));
#18044=CARTESIAN_POINT('Ctrl Pts',(2.29964760564199,0.22023655011824,6.78476839157387));
#18045=CARTESIAN_POINT('Ctrl Pts',(1.06046531360245,2.05236277812793,6.89599410291113));
#18046=CARTESIAN_POINT('Ctrl Pts',(-1.15058580239056,2.00310194380083,7.00721981424842));
#18047=CARTESIAN_POINT('Ctrl Pts',(-2.30733431321409,0.117948200105168,
7.11844552558569));
#18048=CARTESIAN_POINT('Ctrl Pts',(-1.34839894799099,-1.87574608167359,
7.22967123692297));
#18049=CARTESIAN_POINT('Ctrl Pts',(0.845195990122731,-2.1492516091561,7.34089694826023));
#18050=CARTESIAN_POINT('Ctrl Pts',(2.26661351526224,-0.454242447337005,
7.45212265959753));
#18051=CARTESIAN_POINT('Ctrl Pts',(1.60529782693949,1.66030283804416,7.56334837093479));
#18052=CARTESIAN_POINT('Ctrl Pts',(0.190989339949464,2.05048373239734,7.63749884515964));
#18053=CARTESIAN_POINT('Ctrl Pts',(-0.442390676732572,1.90326206528163,
7.67457408227207));
#18054=CARTESIAN_POINT('Ctrl Pts',(-1.95381346134878,-0.0017935399644829,
6.42413030787577));
#18055=CARTESIAN_POINT('Ctrl Pts',(-1.9552538907035,-0.159408210813097,
6.43311729110453));
#18056=CARTESIAN_POINT('Ctrl Pts',(-1.93778561972322,-0.316707681574419,
6.44210427433328));
#18057=CARTESIAN_POINT('Ctrl Pts',(-1.90018450030199,-0.469037744489771,
6.45109125756203));
#18058=CARTESIAN_POINT('Ctrl Pts',(-1.7450634343391,-1.09746588975075,6.48816649467446));
#18059=CARTESIAN_POINT('Ctrl Pts',(-1.24729670772129,-1.64131851955799,
6.52524173178688));
#18060=CARTESIAN_POINT('Ctrl Pts',(-0.635026888167849,-1.85133382266882,
6.56231696889931));
#18061=CARTESIAN_POINT('Ctrl Pts',(-0.02275706861441,-2.06134912577965,
6.59939220601173));
#18062=CARTESIAN_POINT('Ctrl Pts',(0.704015843874659,-1.93752710219408,
6.63646744312416));
#18063=CARTESIAN_POINT('Ctrl Pts',(1.21221210833224,-1.53662581894683,6.67354268023658));
#18064=CARTESIAN_POINT('Ctrl Pts',(1.7204083727898,-1.1357245356996,6.71061791734901));
#18065=CARTESIAN_POINT('Ctrl Pts',(2.01002798921589,-0.457743992790703,
6.74769315446144));
#18066=CARTESIAN_POINT('Ctrl Pts',(1.94830741542236,0.186600649998693,6.78476839157386));
#18067=CARTESIAN_POINT('Ctrl Pts',(1.88658684162883,0.830945292788112,6.82184362868628));
#18068=CARTESIAN_POINT('Ctrl Pts',(1.47352607761564,1.44165403545803,6.85891886579871));
#18069=CARTESIAN_POINT('Ctrl Pts',(0.898487176276873,1.73879826773846,6.89599410291113));
#18070=CARTESIAN_POINT('Ctrl Pts',(0.323448274938114,2.0359425000189,6.93306934002356));
#18071=CARTESIAN_POINT('Ctrl Pts',(-0.413568763726226,2.01952222190986,
6.97014457713599));
#18072=CARTESIAN_POINT('Ctrl Pts',(-0.974868701528982,1.69711979223941,
7.00721981424841));
#18073=CARTESIAN_POINT('Ctrl Pts',(-1.17057269468519,1.58471029663753,7.02014654283228));
#18074=CARTESIAN_POINT('Ctrl Pts',(-1.344915597571,1.43510400955329,7.03307327141614));
#18075=CARTESIAN_POINT('Ctrl Pts',(-1.49039960333529,1.260503289177,7.046));
#18076=CARTESIAN_POINT('Ctrl Pts',(-0.905552056217064,-1.26793026328003,
2.94902990916057E-17));
#18077=CARTESIAN_POINT('Ctrl Pts',(-0.937134822631023,-1.25104249355971,
4.75162406228688E-17));
#18078=CARTESIAN_POINT('Ctrl Pts',(-0.968036761240596,-1.23301924856148,
-1.58634398933136E-16));
#18079=CARTESIAN_POINT('Ctrl Pts',(-0.998189477963827,-1.21387418528302,
-1.99493199737333E-16));
#18080=CARTESIAN_POINT('Ctrl Pts',(-1.04824220989901,-1.18209387411058,
-2.7512401071258E-16));
#18081=CARTESIAN_POINT('Ctrl Pts',(-1.09623172292828,-1.14722531738451,
-1.13947733410607E-16));
#18082=CARTESIAN_POINT('Ctrl Pts',(-1.14207949782356,-1.10958932626875,
-2.28983498828939E-16));
#18083=CARTESIAN_POINT('Ctrl Pts',(-1.16812476791348,-1.08820901815237,
-2.94333182366767E-16));
#18084=CARTESIAN_POINT('Ctrl Pts',(-1.19347860393222,-1.06593466358557,
-2.59231987339497E-16));
#18085=CARTESIAN_POINT('Ctrl Pts',(-1.21812392229353,-1.04281835170969,
-2.1163626406917E-16));
#18086=CARTESIAN_POINT('Ctrl Pts',(-1.23207453972119,-1.02973323677667,
-1.84694444255666E-16));
#18087=CARTESIAN_POINT('Ctrl Pts',(-1.24580226168736,-1.01637377846959,
3.24804729171387E-17));
#18088=CARTESIAN_POINT('Ctrl Pts',(-1.2592797890629,-1.00277371885107,1.38777878078145E-17));
#18089=CARTESIAN_POINT('Ctrl Pts',(-1.30315654392119,-0.95849805423447,
-4.66841707402696E-17));
#18090=CARTESIAN_POINT('Ctrl Pts',(-1.34442524303116,-0.911639949761556,
-4.44200463634023E-16));
#18091=CARTESIAN_POINT('Ctrl Pts',(-1.38299703120573,-0.862548384977714,
-4.09394740330526E-16));
#18092=CARTESIAN_POINT('Ctrl Pts',(-1.41261207961662,-0.824856353147081,
-3.82671240347992E-16));
#18093=CARTESIAN_POINT('Ctrl Pts',(-1.44063702556457,-0.785846462927244,
-3.12176496943412E-16));
#18094=CARTESIAN_POINT('Ctrl Pts',(-1.46702161869435,-0.745658482546257,
-3.67761376907083E-16));
#18095=CARTESIAN_POINT('Ctrl Pts',(-1.48012065014873,-0.725706550124602,
-3.9535733366299E-16));
#18096=CARTESIAN_POINT('Ctrl Pts',(-1.4928152185087,-0.705464023789787,
-1.55640291167757E-16));
#18097=CARTESIAN_POINT('Ctrl Pts',(-1.50509817356396,-0.68494682789941,
-1.17961196366423E-16));
#18098=CARTESIAN_POINT('Ctrl Pts',(-1.5112932288107,-0.674598734832467,
-9.89572943826601E-17));
#18099=CARTESIAN_POINT('Ctrl Pts',(-1.51737856906155,-0.664189090325049,
-2.93080070452884E-16));
#18100=CARTESIAN_POINT('Ctrl Pts',(-1.52335311621856,-0.653721302282831,
-2.77555756156289E-16));
#18101=CARTESIAN_POINT('Ctrl Pts',(-1.55547318924941,-0.597444883744102,
-1.94094684403748E-16));
#18102=CARTESIAN_POINT('Ctrl Pts',(-1.58439860819566,-0.539482552118629,
-3.31420483543467E-16));
#18103=CARTESIAN_POINT('Ctrl Pts',(-1.61003533926912,-0.480187572841947,
-3.19189119579733E-16));
#18104=CARTESIAN_POINT('Ctrl Pts',(-1.63616747730804,-0.419746770969312,
-3.06721395415186E-16));
#18105=CARTESIAN_POINT('Ctrl Pts',(-1.65888335052524,-0.357920523309995,
-2.80209762252872E-16));
#18106=CARTESIAN_POINT('Ctrl Pts',(-1.67804895967927,-0.295042072125015,
-1.66533453693773E-16));
#18107=CARTESIAN_POINT('Ctrl Pts',(-1.69039160882678,-0.254548359888778,
-9.33259296514283E-17));
#18108=CARTESIAN_POINT('Ctrl Pts',(-1.70126111007635,-0.213617460141972,
-2.30505991696603E-16));
#18109=CARTESIAN_POINT('Ctrl Pts',(-1.71061208520917,-0.172332131165316,
-2.91433543964104E-16));
#18110=CARTESIAN_POINT('Ctrl Pts',(-1.715816487101,-0.149354266164202,-3.2534353343379E-16));
#18111=CARTESIAN_POINT('Ctrl Pts',(-1.72055036402814,-0.126266539334649,
-1.00298932279788E-16));
#18112=CARTESIAN_POINT('Ctrl Pts',(-1.72480472543126,-0.103082789841687,
-9.71445146547012E-17));
#18113=CARTESIAN_POINT('Ctrl Pts',(-1.72695538876364,-0.0913629486676286,
-9.55498945276206E-17));
#18114=CARTESIAN_POINT('Ctrl Pts',(-1.72898375858757,-0.07961694527504,
-1.96680959500023E-16));
#18115=CARTESIAN_POINT('Ctrl Pts',(-1.73088777000182,-0.0678516147389183,
-1.94289029309402E-16));
#18116=CARTESIAN_POINT('Ctrl Pts',(-1.74172080812434,-0.000911745960731708,
-1.80679934979654E-16));
#18117=CARTESIAN_POINT('Ctrl Pts',(-1.74848760095285,0.0663732156671881,
-2.27318435210151E-17));
#18118=CARTESIAN_POINT('Ctrl Pts',(-1.75106859893149,0.133645381706535,
-4.16333634234434E-17));
#18119=CARTESIAN_POINT('Ctrl Pts',(-1.75197360252239,0.157233758116401,
-4.82610103750263E-17));
#18120=CARTESIAN_POINT('Ctrl Pts',(-1.75236359562623,0.180820850215305,
-8.28170566717793E-17));
#18121=CARTESIAN_POINT('Ctrl Pts',(-1.75223214201128,0.204392038445102,
-5.55111512312578E-17));
#18122=CARTESIAN_POINT('Ctrl Pts',(-1.75187057279805,0.269225675666801,
2.10533692500149E-17));
#18123=CARTESIAN_POINT('Ctrl Pts',(-1.74756789056806,0.333938320850628,
-1.60420900056E-17));
#18124=CARTESIAN_POINT('Ctrl Pts',(-1.73954116331082,0.398294466418659,
0.));
#18125=CARTESIAN_POINT('Ctrl Pts',(-1.73091740426649,0.467437452671242,
1.72353082822116E-17));
#18126=CARTESIAN_POINT('Ctrl Pts',(-1.71799540177027,0.536169874708505,
-4.36478159584899E-17));
#18127=CARTESIAN_POINT('Ctrl Pts',(-1.70098034075862,0.604204029641736,
8.32667268468867E-17));
#18128=CARTESIAN_POINT('Ctrl Pts',(-1.69824130486499,0.615155973465351,
1.03697067233541E-16));
#18129=CARTESIAN_POINT('Ctrl Pts',(-1.69539827041295,0.626080961021427,
1.29813171089747E-16));
#18130=CARTESIAN_POINT('Ctrl Pts',(-1.69245305315959,0.636975805303662,
1.11022302462516E-16));
#18131=CARTESIAN_POINT('Ctrl Pts',(-1.67473398681781,0.702521553550295,
-2.02764230671151E-18));
#18132=CARTESIAN_POINT('Ctrl Pts',(-1.65331496860816,0.766998932259627,
-2.57263159617093E-16));
#18133=CARTESIAN_POINT('Ctrl Pts',(-1.62845169327078,0.83015154980978,-1.94289029309402E-16));
#18134=CARTESIAN_POINT('Ctrl Pts',(-1.60307671281799,0.894603896257815,
-1.30018843507023E-16));
#18135=CARTESIAN_POINT('Ctrl Pts',(-1.57411406965586,0.957677277748301,
-1.42237185085071E-16));
#18136=CARTESIAN_POINT('Ctrl Pts',(-1.54178048300264,1.01910167818773,-5.55111512312578E-17));
#18137=CARTESIAN_POINT('Ctrl Pts',(-1.50922784853364,1.08094220569947,3.18024186880875E-17));
#18138=CARTESIAN_POINT('Ctrl Pts',(-1.47325811155629,1.14111231916335,-1.86023089836484E-16));
#18139=CARTESIAN_POINT('Ctrl Pts',(-1.43404118681899,1.19932479720781,-1.66533453693773E-16));
#18140=CARTESIAN_POINT('Ctrl Pts',(-1.42513259519695,1.21254845504633,-1.62106150675484E-16));
#18141=CARTESIAN_POINT('Ctrl Pts',(-1.41605624454103,1.22567101155683,-3.77067070771252E-16));
#18142=CARTESIAN_POINT('Ctrl Pts',(-1.40681378949184,1.23868893327645,-3.88578058618805E-16));
#18143=CARTESIAN_POINT('Ctrl Pts',(-1.40005105796202,1.24821418486786,-3.97000682266051E-16));
#18144=CARTESIAN_POINT('Ctrl Pts',(-1.39319940015811,1.25768325768832,-4.06719094166719E-16));
#18145=CARTESIAN_POINT('Ctrl Pts',(-1.3862680939899,1.26708342641975,-3.88578058618805E-16));
#18146=CARTESIAN_POINT('Ctrl Pts',(-1.34342259960335,1.32519006127916,-2.76440228046676E-16));
#18147=CARTESIAN_POINT('Ctrl Pts',(-1.2974598126633,1.38077597290076,-1.69458509682717E-16));
#18148=CARTESIAN_POINT('Ctrl Pts',(-1.24862081372783,1.43356038861728,-1.94289029309402E-16));
#18149=CARTESIAN_POINT('Ctrl Pts',(-1.19966911793571,1.48646660530969,-2.19176845800727E-16));
#18150=CARTESIAN_POINT('Ctrl Pts',(-1.14782748930566,1.53655939185262,-1.74330404157582E-16));
#18151=CARTESIAN_POINT('Ctrl Pts',(-1.09328907277386,1.5835398262669,-5.55111512312578E-17));
#18152=CARTESIAN_POINT('Ctrl Pts',(-1.03991703070208,1.62951552342795,6.07669985463979E-17));
#18153=CARTESIAN_POINT('Ctrl Pts',(-0.983961746585148,1.67251142482066,
1.56834561468643E-16));
#18154=CARTESIAN_POINT('Ctrl Pts',(-0.925564466602708,1.71221823957964,
2.22044604925031E-16));
#18155=CARTESIAN_POINT('Ctrl Pts',(-0.904533489913129,1.72651810244765,
2.45529104618684E-16));
#18156=CARTESIAN_POINT('Ctrl Pts',(-0.883185451447723,1.74039103644132,
-1.04689938393391E-17));
#18157=CARTESIAN_POINT('Ctrl Pts',(-0.861525859670525,1.75382131162755,
0.));
#18158=CARTESIAN_POINT('Origin',(0.,0.,0.));
#18159=CARTESIAN_POINT('Origin',(-0.866025403784439,-1.5,-4.));
#18160=CARTESIAN_POINT('',(-0.866025403784439,-1.5,-4.));
#18161=CARTESIAN_POINT('',(0.866025403784439,-1.5,-4.));
#18162=CARTESIAN_POINT('',(-0.43301270189222,-1.5,-4.));
#18163=CARTESIAN_POINT('',(-0.866025403784439,-1.5,-2.));
#18164=CARTESIAN_POINT('',(-0.866025403784439,-1.5,-4.));
#18165=CARTESIAN_POINT('',(0.866025403784439,-1.5,-2.));
#18166=CARTESIAN_POINT('',(-0.866025403784439,-1.5,-2.));
#18167=CARTESIAN_POINT('',(0.866025403784439,-1.5,-4.));
#18168=CARTESIAN_POINT('Origin',(-1.73205080756888,2.12115047744981E-16,
-4.));
#18169=CARTESIAN_POINT('',(-1.73205080756888,2.12115047744981E-16,-4.));
#18170=CARTESIAN_POINT('',(-1.51554445662277,-0.375,-4.));
#18171=CARTESIAN_POINT('',(-1.73205080756888,2.77555756156289E-16,-2.));
#18172=CARTESIAN_POINT('',(-1.73205080756888,2.12115047744981E-16,-4.));
#18173=CARTESIAN_POINT('',(-1.73205080756888,2.12115047744981E-16,-2.));
#18174=CARTESIAN_POINT('Origin',(-0.866025403784438,1.5,-4.));
#18175=CARTESIAN_POINT('',(-0.866025403784438,1.5,-4.));
#18176=CARTESIAN_POINT('',(-1.08253175473055,1.125,-4.));
#18177=CARTESIAN_POINT('',(-0.866025403784438,1.5,-2.));
#18178=CARTESIAN_POINT('',(-0.866025403784438,1.5,-4.));
#18179=CARTESIAN_POINT('',(-0.866025403784438,1.5,-2.));
#18180=CARTESIAN_POINT('Origin',(0.866025403784439,1.5,-4.));
#18181=CARTESIAN_POINT('',(0.866025403784439,1.5,-4.));
#18182=CARTESIAN_POINT('',(0.43301270189222,1.5,-4.));
#18183=CARTESIAN_POINT('',(0.866025403784439,1.5,-2.));
#18184=CARTESIAN_POINT('',(0.866025403784439,1.5,-4.));
#18185=CARTESIAN_POINT('',(0.866025403784439,1.5,-2.));
#18186=CARTESIAN_POINT('Origin',(1.73205080756888,0.,-4.));
#18187=CARTESIAN_POINT('',(1.73205080756888,0.,-4.));
#18188=CARTESIAN_POINT('',(1.51554445662277,0.375,-4.));
#18189=CARTESIAN_POINT('',(1.73205080756888,0.,-2.));
#18190=CARTESIAN_POINT('',(1.73205080756888,0.,-4.));
#18191=CARTESIAN_POINT('',(1.73205080756888,0.,-2.));
#18192=CARTESIAN_POINT('Origin',(0.866025403784439,-1.5,-4.));
#18193=CARTESIAN_POINT('',(1.08253175473055,-1.125,-4.));
#18194=CARTESIAN_POINT('',(0.866025403784439,-1.5,-2.));
#18195=CARTESIAN_POINT('Origin',(0.,2.77555756156289E-16,-2.));
#18196=CARTESIAN_POINT('Origin',(0.,0.,0.));
#18197=CARTESIAN_POINT('',(-3.5,-4.28626379701574E-16,0.));
#18198=CARTESIAN_POINT('Origin',(0.,0.,0.));
#18199=CARTESIAN_POINT('Origin',(0.,0.,-4.));
#18200=CARTESIAN_POINT('',(-3.5,-4.28626379701574E-16,-4.));
#18201=CARTESIAN_POINT('',(-3.5,-4.28626379701574E-16,-4.));
#18202=CARTESIAN_POINT('Origin',(0.,0.,-4.));
#18203=CARTESIAN_POINT('Origin',(0.,0.,-4.));
#18204=CARTESIAN_POINT('Origin',(0.,0.,8.));
#21864=UNCERTAINTY_MEASURE_WITH_UNIT(LENGTH_MEASURE(0.01),#21881,
'DISTANCE_ACCURACY_VALUE',
'Maximum model space distance between geometric entities at asserted c
onnectivities');
#21868=UNCERTAINTY_MEASURE_WITH_UNIT(LENGTH_MEASURE(0.01),#21881,
'DISTANCE_ACCURACY_VALUE',
'Maximum model space distance between geometric entities at asserted c
onnectivities');
#21876=(
GEOMETRIC_REPRESENTATION_CONTEXT(3)
GLOBAL_UNCERTAINTY_ASSIGNED_CONTEXT((#21864))
GLOBAL_UNIT_ASSIGNED_CONTEXT((#21881,#21883,#21884))
REPRESENTATION_CONTEXT('','3D')
);
#21880=(
GEOMETRIC_REPRESENTATION_CONTEXT(3)
GLOBAL_UNCERTAINTY_ASSIGNED_CONTEXT((#21868))
GLOBAL_UNIT_ASSIGNED_CONTEXT((#21881,#21883,#21884))
REPRESENTATION_CONTEXT('','3D')
);
#21881=(
LENGTH_UNIT()
NAMED_UNIT(*)
SI_UNIT(.MILLI.,.METRE.)
);
#21883=(
NAMED_UNIT(*)
PLANE_ANGLE_UNIT()
SI_UNIT($,.RADIAN.)
);
#21884=(
NAMED_UNIT(*)
SI_UNIT($,.STERADIAN.)
SOLID_ANGLE_UNIT()
);
#21892=SHAPE_DEFINITION_REPRESENTATION(#21903,#21931);
#21903=PRODUCT_DEFINITION_SHAPE('',$,#21943);
#21931=SHAPE_REPRESENTATION('',(#6822),#21876);
#21935=PRODUCT_DEFINITION_CONTEXT('part definition',#21970,'design');
#21943=PRODUCT_DEFINITION('Socket head cap screw M4x8',
'Socket head cap screw M4x8',#21954,#21935);
#21954=PRODUCT_DEFINITION_FORMATION('',$,#21979);
#21970=APPLICATION_CONTEXT(
'Core Data for Automotive Mechanical Design Process');
#21971=PRODUCT_CONTEXT('part definition',#21970,'mechanical');
#21979=PRODUCT('Socket head cap screw M4x8',
'Socket head cap screw M4x8',$,(#21971));
#21986=PRESENTATION_STYLE_ASSIGNMENT((#21992));
#21992=SURFACE_STYLE_USAGE(.BOTH.,#21998);
#21998=SURFACE_SIDE_STYLE('',(#22004));
#22004=SURFACE_STYLE_FILL_AREA(#22010);
#22010=FILL_AREA_STYLE('Dark gray',(#22016));
#22016=FILL_AREA_STYLE_COLOUR('Dark gray',#22022);
#22022=COLOUR_RGB('Dark gray',0.250980392156863,0.282352941176471,0.32156862745098);
ENDSEC;
END-ISO-10303-21;
